ISO-10303-21;
HEADER;
FILE_DESCRIPTION (('STEP AP214'),
    '1' );
FILE_NAME ('Bracket washer.step',
    '2026-10-06T08:09:25',
    ( '' ),
    ( '' ),
    'SwSTEP 2.0',
    'SolidWorks 2021',
    '' );
FILE_SCHEMA (( 'AUTOMOTIVE_DESIGN' ));
ENDSEC;

DATA;
#26=AXIS2_PLACEMENT_3D ( 'NONE', #18449, #2330, #9512 ) ;
#42=CARTESIAN_POINT ( 'NONE',  ( 0.2500000000000071609, 2.000000000000001776, -0.2500000000000002220 ) ) ;
#52=EDGE_CURVE ( 'NONE', #21352, #10482, #865, .T. ) ;
#58=ORIENTED_EDGE ( 'NONE', *, *, #7145, .T. ) ;
#62=ORIENTED_EDGE ( 'NONE', *, *, #144, .F. ) ;
#68=CARTESIAN_POINT ( 'NONE',  ( 12.49999999999995914, 2.775557561562891982E-14, -4.500000000000002665 ) ) ;
#76=VECTOR ( 'NONE', #7557, 1000.000000000000000 ) ;
#109=FACE_OUTER_BOUND ( 'NONE', #9678, .T. ) ;
#114=ORIENTED_EDGE ( 'NONE', *, *, #778, .F. ) ;
#132=CARTESIAN_POINT ( 'NONE',  ( 25.00000000000000355, 2.000000000000001776, -1.250000000000004663 ) ) ;
#144=EDGE_CURVE ( 'NONE', #13324, #19219, #20095, .T. ) ;
#187=CARTESIAN_POINT ( 'NONE',  ( 24.99999999999998934, 1.500000000000001332, -2.000000000000005329 ) ) ;
#223=DIRECTION ( 'NONE',  ( -1.066786462891689527E-26, -6.656013887802287108E-31, -1.000000000000000000 ) ) ;
#269=CARTESIAN_POINT ( 'NONE',  ( -1.734723475976807094E-14, 1.250000000000001110, -17.00000000000000711 ) ) ;
#282=AXIS2_PLACEMENT_3D ( 'NONE', #9971, #20557, #10084 ) ;
#295=CIRCLE ( 'NONE', #11546, 0.2500000000000003331 ) ;
#320=CYLINDRICAL_SURFACE ( 'NONE', #22884, 0.2500000000000000000 ) ;
#342=DIRECTION ( 'NONE',  ( -1.000000000000000000, -3.254448077276381206E-32, -1.066788928082016908E-26 ) ) ;
#346=CARTESIAN_POINT ( 'NONE',  ( 1.040834085586084257E-14, 4.500000000000003553, -1.499999999999994449 ) ) ;
#365=VECTOR ( 'NONE', #7293, 1000.000000000000000 ) ;
#366=ADVANCED_FACE ( 'NONE', ( #833 ), #7887, .F. ) ;
#399=ORIENTED_EDGE ( 'NONE', *, *, #12220, .F. ) ;
#433=DIRECTION ( 'NONE',  ( -1.000000000000000000, -3.254448077276381206E-32, -1.066788928082016908E-26 ) ) ;
#434=DIRECTION ( 'NONE',  ( -1.000000000000000000, -3.254448077276381206E-32, -1.066788928082016908E-26 ) ) ;
#440=CARTESIAN_POINT ( 'NONE',  ( 12.49999999999995914, 1.250000000000015099, -14.25000000000000178 ) ) ;
#449=LINE ( 'NONE', #2321, #365 ) ;
#482=EDGE_LOOP ( 'NONE', ( #12383, #18200, #19111, #4814 ) ) ;
#491=PLANE ( 'NONE',  #4882 ) ;
#493=CARTESIAN_POINT ( 'NONE',  ( 24.74999999999999645, 0.2500000000000418554, -17.00000000000001066 ) ) ;
#503=LINE ( 'NONE', #14843, #76 ) ;
#515=ORIENTED_EDGE ( 'NONE', *, *, #15969, .F. ) ;
#531=LINE ( 'NONE', #7924, #22271 ) ;
#546=EDGE_LOOP ( 'NONE', ( #13785, #3691, #515, #3410 ) ) ;
#598=ORIENTED_EDGE ( 'NONE', *, *, #9835, .F. ) ;
#606=CARTESIAN_POINT ( 'NONE',  ( 12.49999999999997335, 1.500000000000015099, -9.500000000000001776 ) ) ;
#616=FACE_BOUND ( 'NONE', #9219, .T. ) ;
#627=ORIENTED_EDGE ( 'NONE', *, *, #1615, .F. ) ;
#654=CARTESIAN_POINT ( 'NONE',  ( 0.2499999999999655276, 2.000000000000015543, -2.000000000000001776 ) ) ;
#657=EDGE_LOOP ( 'NONE', ( #7151, #5646, #14168, #8629 ) ) ;
#659=AXIS2_PLACEMENT_3D ( 'NONE', #20444, #3967, #5749 ) ;
#660=ORIENTED_EDGE ( 'NONE', *, *, #16140, .T. ) ;
#661=AXIS2_PLACEMENT_3D ( 'NONE', #4718, #969, #19185 ) ;
#682=AXIS2_PLACEMENT_3D ( 'NONE', #19335, #4745, #4857 ) ;
#696=FACE_OUTER_BOUND ( 'NONE', #6302, .T. ) ;
#753=ORIENTED_EDGE ( 'NONE', *, *, #1882, .T. ) ;
#778=EDGE_CURVE ( 'NONE', #20423, #3633, #5417, .T. ) ;
#800=VERTEX_POINT ( 'NONE', #7297 ) ;
#811=EDGE_CURVE ( 'NONE', #17281, #16004, #992, .T. ) ;
#823=CARTESIAN_POINT ( 'NONE',  ( 2.499999999999971134, 4.250000000000003553, -1.500000000000029088 ) ) ;
#826=ORIENTED_EDGE ( 'NONE', *, *, #17744, .F. ) ;
#833=FACE_OUTER_BOUND ( 'NONE', #12010, .T. ) ;
#846=FACE_OUTER_BOUND ( 'NONE', #19731, .T. ) ;
#865=LINE ( 'NONE', #22739, #9193 ) ;
#874=CARTESIAN_POINT ( 'NONE',  ( 0.2500000000000036637, 2.000000000000001776, -17.00000000000000711 ) ) ;
#879=LINE ( 'NONE', #16966, #14230 ) ;
#882=VERTEX_POINT ( 'NONE', #18567 ) ;
#908=CARTESIAN_POINT ( 'NONE',  ( 2.499999999999992006, 4.250000000000003553, -3.469446951953614189E-14 ) ) ;
#910=AXIS2_PLACEMENT_3D ( 'NONE', #13957, #10664, #16064 ) ;
#917=FACE_OUTER_BOUND ( 'NONE', #16745, .T. ) ;
#924=EDGE_CURVE ( 'NONE', #20683, #3062, #16438, .T. ) ;
#945=DIRECTION ( 'NONE',  ( 3.254448077146059901E-32, 1.000000000000000000, 6.409494854920712161E-31 ) ) ;
#947=PLANE ( 'NONE',  #15243 ) ;
#968=FACE_OUTER_BOUND ( 'NONE', #14289, .T. ) ;
#969=DIRECTION ( 'NONE',  ( 1.000000000000000000, 3.254448077276381206E-32, 1.066788928082016908E-26 ) ) ;
#991=DIRECTION ( 'NONE',  ( -1.066786462891689527E-26, -6.656013887802287108E-31, -1.000000000000000000 ) ) ;
#992=CIRCLE ( 'NONE', #11118, 0.2500000000000002220 ) ;
#1011=ORIENTED_EDGE ( 'NONE', *, *, #18784, .T. ) ;
#1029=DIRECTION ( 'NONE',  ( 0.000000000000000000, 0.000000000000000000, -1.000000000000000000 ) ) ;
#1079=CARTESIAN_POINT ( 'NONE',  ( 2.499999999999998668, 2.000000000000001776, -17.75000000000000711 ) ) ;
#1094=FACE_OUTER_BOUND ( 'NONE', #18101, .T. ) ;
#1102=ORIENTED_EDGE ( 'NONE', *, *, #20925, .T. ) ;
#1104=VERTEX_POINT ( 'NONE', #18803 ) ;
#1120=CARTESIAN_POINT ( 'NONE',  ( 12.49999999999995914, 2.775557561562891351E-14, -9.500000000000003553 ) ) ;
#1135=DIRECTION ( 'NONE',  ( 1.000000000000000000, 0.000000000000000000, 0.000000000000000000 ) ) ;
#1162=DIRECTION ( 'NONE',  ( -1.066786462891689527E-26, -6.656013887802287108E-31, -1.000000000000000000 ) ) ;
#1165=DIRECTION ( 'NONE',  ( 1.066786462891689527E-26, 6.656013887802287108E-31, 1.000000000000000000 ) ) ;
#1183=CARTESIAN_POINT ( 'NONE',  ( 24.74999999999996447, 1.500000000000043077, -2.000000000000005329 ) ) ;
#1189=TOROIDAL_SURFACE ( 'NONE', #11309, 2.250000000000000444, 0.2500000000000000000 ) ;
#1233=PRODUCT_DEFINITION_SHAPE ( 'NONE', 'NONE',  #14519 ) ;
#1275=VERTEX_POINT ( 'NONE', #11670 ) ;
#1281=CIRCLE ( 'NONE', #14424, 0.2500000000000003331 ) ;
#1308=CIRCLE ( 'NONE', #3557, 0.7500000000000006661 ) ;
#1340=DIRECTION ( 'NONE',  ( 1.000000000000000000, 3.254448077276381206E-32, 1.066788928082016908E-26 ) ) ;
#1359=DIRECTION ( 'NONE',  ( -1.000000000000000000, 0.000000000000000000, -1.066194817212772764E-26 ) ) ;
#1419=DIRECTION ( 'NONE',  ( -1.064962222048364933E-26, 0.000000000000000000, -1.000000000000000000 ) ) ;
#1460=AXIS2_PLACEMENT_3D ( 'NONE', #13839, #22554, #6324 ) ;
#1512=CARTESIAN_POINT ( 'NONE',  ( 25.00000000000001066, 0.2500000000000002220, -17.00000000000001066 ) ) ;
#1523=FACE_OUTER_BOUND ( 'NONE', #22735, .T. ) ;
#1527=CARTESIAN_POINT ( 'NONE',  ( 24.99999999999999645, 0.2499999999999863443, -19.00000000000001421 ) ) ;
#1576=ORIENTED_EDGE ( 'NONE', *, *, #15133, .F. ) ;
#1600=VECTOR ( 'NONE', #21371, 1000.000000000000000 ) ;
#1608=ORIENTED_EDGE ( 'NONE', *, *, #15687, .F. ) ;
#1615=EDGE_CURVE ( 'NONE', #16004, #5080, #8970, .T. ) ;
#1647=CARTESIAN_POINT ( 'NONE',  ( 22.49999999999999645, 4.250000000000031974, -2.081668171172168513E-14 ) ) ;
#1653=CARTESIAN_POINT ( 'NONE',  ( 2.499999999999960476, 4.500000000000017764, -18.75000000000002132 ) ) ;
#1654=CARTESIAN_POINT ( 'NONE',  ( 25.00000000000000355, 2.000000000000001776, -0.2500000000000002220 ) ) ;
#1659=EDGE_CURVE ( 'NONE', #5612, #5080, #16736, .T. ) ;
#1742=EDGE_CURVE ( 'NONE', #10482, #16513, #19865, .T. ) ;
#1751=CIRCLE ( 'NONE', #20541, 4.750000000000000888 ) ;
#1774=VERTEX_POINT ( 'NONE', #13656 ) ;
#1776=AXIS2_PLACEMENT_3D ( 'NONE', #8921, #13973, #7050 ) ;
#1806=ORIENTED_EDGE ( 'NONE', *, *, #14276, .F. ) ;
#1819=DIRECTION ( 'NONE',  ( 1.000000000000000000, 3.254448077276381206E-32, 1.066788928082016908E-26 ) ) ;
#1825=AXIS2_PLACEMENT_3D ( 'NONE', #606, #12956, #7769 ) ;
#1855=ORIENTED_EDGE ( 'NONE', *, *, #16854, .T. ) ;
#1879=EDGE_CURVE ( 'NONE', #7941, #3485, #4038, .T. ) ;
#1882=EDGE_CURVE ( 'NONE', #11578, #13234, #10444, .T. ) ;
#1927=AXIS2_PLACEMENT_3D ( 'NONE', #3972, #342, #7738 ) ;
#1939=ORIENTED_EDGE ( 'NONE', *, *, #20832, .F. ) ;
#1941=AXIS2_PLACEMENT_3D ( 'NONE', #11300, #14717, #8769 ) ;
#1942=AXIS2_PLACEMENT_3D ( 'NONE', #17252, #1165, #19145 ) ;
#1945=EDGE_LOOP ( 'NONE', ( #11982, #5081, #22904, #18569 ) ) ;
#1957=DIRECTION ( 'NONE',  ( -1.000000000000000000, -3.254448077276381206E-32, -1.066788928082016908E-26 ) ) ;
#1963=CYLINDRICAL_SURFACE ( 'NONE', #11964, 0.5000000000000004441 ) ;
#1973=VECTOR ( 'NONE', #19204, 1000.000000000000000 ) ;
#1989=DIRECTION ( 'NONE',  ( 0.000000000000000000, 0.000000000000000000, 1.000000000000000000 ) ) ;
#2012=DIRECTION ( 'NONE',  ( 0.000000000000000000, 0.000000000000000000, -1.000000000000000000 ) ) ;
#2031=ORIENTED_EDGE ( 'NONE', *, *, #6558, .T. ) ;
#2059=EDGE_LOOP ( 'NONE', ( #13155, #15519, #10163, #5816 ) ) ;
#2088=FACE_OUTER_BOUND ( 'NONE', #546, .T. ) ;
#2090=MECHANICAL_DESIGN_GEOMETRIC_PRESENTATION_REPRESENTATION('',(#7610),#17491);
#2124=DIRECTION ( 'NONE',  ( 1.066786462891689527E-26, 6.656013887802287108E-31, 1.000000000000000000 ) ) ;
#2160=VECTOR ( 'NONE', #21970, 1000.000000000000000 ) ;
#2167=ADVANCED_FACE ( 'NONE', ( #11162 ), #13167, .F. ) ;
#2168=CARTESIAN_POINT ( 'NONE',  ( 0.2499999999999967526, 1.250000000000042633, -17.00000000000000711 ) ) ;
#2175=EDGE_LOOP ( 'NONE', ( #20129, #22994, #7714, #4335 ) ) ;
#2186=ORIENTED_EDGE ( 'NONE', *, *, #21785, .T. ) ;
#2206=CARTESIAN_POINT ( 'NONE',  ( 22.49999999999998224, 2.000000000000001776, -0.2500000000000210387 ) ) ;
#2217=DIRECTION ( 'NONE',  ( -1.066786462891689527E-26, -6.656013887802287108E-31, -1.000000000000000000 ) ) ;
#2242=VERTEX_POINT ( 'NONE', #13512 ) ;
#2272=AXIS2_PLACEMENT_3D ( 'NONE', #42, #10841, #2012 ) ;
#2305=LINE ( 'NONE', #908, #4186 ) ;
#2321=CARTESIAN_POINT ( 'NONE',  ( 22.49999999999996092, 4.500000000000073719, -17.74999999999998224 ) ) ;
#2328=LINE ( 'NONE', #14915, #12088 ) ;
#2329=EDGE_CURVE ( 'NONE', #14364, #16088, #4812, .T. ) ;
#2330=DIRECTION ( 'NONE',  ( 1.000000000000000000, 3.254448077276381206E-32, 1.066788928082016908E-26 ) ) ;
#2340=CARTESIAN_POINT ( 'NONE',  ( -1.734723475976807094E-14, 2.000000000000001776, -17.00000000000000711 ) ) ;
#2376=PRESENTATION_STYLE_ASSIGNMENT (( #20273 ) ) ;
#2417=AXIS2_PLACEMENT_3D ( 'NONE', #10499, #19435, #18141 ) ;
#2423=CARTESIAN_POINT ( 'NONE',  ( 24.99999999999995737, 2.000000000000001776, -16.99999999999999289 ) ) ;
#2432=AXIS2_PLACEMENT_3D ( 'NONE', #14001, #5426, #1419 ) ;
#2440=EDGE_LOOP ( 'NONE', ( #2874, #16973, #17073, #19665 ) ) ;
#2473=ORIENTED_EDGE ( 'NONE', *, *, #16535, .F. ) ;
#2503=EDGE_LOOP ( 'NONE', ( #9497, #6072, #10283, #14107 ) ) ;
#2510=CARTESIAN_POINT ( 'NONE',  ( 2.499999999999960476, 4.500000000000017764, -18.75000000000002132 ) ) ;
#2515=CARTESIAN_POINT ( 'NONE',  ( 0.2500000000000036637, 2.000000000000001776, -17.00000000000000711 ) ) ;
#2520=ORIENTED_EDGE ( 'NONE', *, *, #16854, .F. ) ;
#2527=ADVANCED_FACE ( 'NONE', ( #9725 ), #320, .T. ) ;
#2553=ORIENTED_EDGE ( 'NONE', *, *, #1879, .T. ) ;
#2662=DIRECTION ( 'NONE',  ( 1.066786462891689527E-26, 6.656013887802287108E-31, 1.000000000000000000 ) ) ;
#2676=DIRECTION ( 'NONE',  ( -1.000000000000000000, 0.000000000000000000, -1.066687855278535322E-26 ) ) ;
#2700=DIRECTION ( 'NONE',  ( -1.000000000000000000, 7.100545512326564696E-57, 1.066786462891689527E-26 ) ) ;
#2707=CIRCLE ( 'NONE', #14736, 5.000000000000000888 ) ;
#2733=AXIS2_PLACEMENT_3D ( 'NONE', #18854, #2739, #4616 ) ;
#2739=DIRECTION ( 'NONE',  ( -1.000000000000000000, -3.254448077276381206E-32, -1.066788928082016908E-26 ) ) ;
#2741=CARTESIAN_POINT ( 'NONE',  ( 0.2500000000000036637, 1.387778780781445676E-14, -19.00000000000001066 ) ) ;
#2742=LINE ( 'NONE', #2510, #17374 ) ;
#2763=TOROIDAL_SURFACE ( 'NONE', #5779, 2.250000000000000444, 0.2500000000000000000 ) ;
#2783=CARTESIAN_POINT ( 'NONE',  ( 1.040834085586084257E-14, 4.500000000000003553, 0.000000000000000000 ) ) ;
#2785=CARTESIAN_POINT ( 'NONE',  ( 12.49999999999996625, 0.2500000000000002220, -9.500000000000003553 ) ) ;
#2831=CARTESIAN_POINT ( 'NONE',  ( 22.49999999999999645, 4.250000000000031974, -1.499999999999997780 ) ) ;
#2874=ORIENTED_EDGE ( 'NONE', *, *, #21596, .T. ) ;
#2892=ADVANCED_FACE ( 'NONE', ( #10413 ), #19109, .T. ) ;
#2951=DIRECTION ( 'NONE',  ( 0.000000000000000000, 0.000000000000000000, 1.000000000000000000 ) ) ;
#2960=CIRCLE ( 'NONE', #14974, 2.250000000000003553 ) ;
#2963=DIRECTION ( 'NONE',  ( 0.000000000000000000, 0.000000000000000000, 1.000000000000000000 ) ) ;
#2972=ORIENTED_EDGE ( 'NONE', *, *, #3067, .F. ) ;
#2986=DIRECTION ( 'NONE',  ( 0.000000000000000000, 0.000000000000000000, 1.000000000000000000 ) ) ;
#3007=ORIENTED_EDGE ( 'NONE', *, *, #11484, .F. ) ;
#3035=FACE_OUTER_BOUND ( 'NONE', #12793, .T. ) ;
#3039=DIRECTION ( 'NONE',  ( -1.000000000000000000, 0.000000000000000000, 0.000000000000000000 ) ) ;
#3048=DIRECTION ( 'NONE',  ( -1.066786462891689527E-26, -6.656013887802287108E-31, -1.000000000000000000 ) ) ;
#3054=ORIENTED_EDGE ( 'NONE', *, *, #52, .T. ) ;
#3062=VERTEX_POINT ( 'NONE', #8401 ) ;
#3066=CARTESIAN_POINT ( 'NONE',  ( 24.75000000000000355, 2.000000000000029310, -2.000000000000005329 ) ) ;
#3067=EDGE_CURVE ( 'NONE', #16088, #15251, #9680, .T. ) ;
#3102=CIRCLE ( 'NONE', #14011, 2.250000000000003553 ) ;
#3104=AXIS2_PLACEMENT_3D ( 'NONE', #2423, #433, #10891 ) ;
#3150=ORIENTED_EDGE ( 'NONE', *, *, #1742, .T. ) ;
#3234=ADVANCED_FACE ( 'NONE', ( #18580 ), #13052, .F. ) ;
#3246=ORIENTED_EDGE ( 'NONE', *, *, #11348, .T. ) ;
#3264=ORIENTED_EDGE ( 'NONE', *, *, #13555, .F. ) ;
#3266=EDGE_CURVE ( 'NONE', #4468, #5612, #16793, .T. ) ;
#3296=AXIS2_PLACEMENT_3D ( 'NONE', #3066, #8478, #2951 ) ;
#3325=ORIENTED_EDGE ( 'NONE', *, *, #14140, .F. ) ;
#3370=DIRECTION ( 'NONE',  ( 0.000000000000000000, 0.000000000000000000, 1.000000000000000000 ) ) ;
#3387=EDGE_LOOP ( 'NONE', ( #14017, #3325, #21955, #10024 ) ) ;
#3410=ORIENTED_EDGE ( 'NONE', *, *, #15391, .T. ) ;
#3442=DIRECTION ( 'NONE',  ( -1.066786462891689527E-26, -6.656013887802287108E-31, -1.000000000000000000 ) ) ;
#3474=( LENGTH_UNIT ( ) NAMED_UNIT ( * ) SI_UNIT ( .MILLI., .METRE. ) );
#3484=FACE_OUTER_BOUND ( 'NONE', #9188, .T. ) ;
#3485=VERTEX_POINT ( 'NONE', #11970 ) ;
#3535=CARTESIAN_POINT ( 'NONE',  ( 12.49999999999992362, 1.500000000000015099, -14.49999999999999822 ) ) ;
#3540=AXIS2_PLACEMENT_3D ( 'NONE', #22902, #8775, #8892 ) ;
#3546=DIRECTION ( 'NONE',  ( -1.000000000000000000, -3.254448077276381206E-32, -1.066788928082016908E-26 ) ) ;
#3557=AXIS2_PLACEMENT_3D ( 'NONE', #2340, #7414, #14926 ) ;
#3583=ORIENTED_EDGE ( 'NONE', *, *, #7960, .F. ) ;
#3604=ORIENTED_EDGE ( 'NONE', *, *, #811, .T. ) ;
#3633=VERTEX_POINT ( 'NONE', #1512 ) ;
#3670=DIRECTION ( 'NONE',  ( -1.000000000000000000, -3.254448077276381206E-32, -1.066788928082016908E-26 ) ) ;
#3688=CIRCLE ( 'NONE', #22842, 5.000000000000000888 ) ;
#3691=ORIENTED_EDGE ( 'NONE', *, *, #9989, .T. ) ;
#3732=DIRECTION ( 'NONE',  ( -1.000000000000000000, -3.254448077276381206E-32, -1.066788928082016908E-26 ) ) ;
#3766=EDGE_CURVE ( 'NONE', #10170, #12123, #7498, .T. ) ;
#3798=ORIENTED_EDGE ( 'NONE', *, *, #4187, .T. ) ;
#3805=ORIENTED_EDGE ( 'NONE', *, *, #144, .T. ) ;
#3864=CARTESIAN_POINT ( 'NONE',  ( 22.50000000000003908, 4.500000000000031974, -1.499999999999997780 ) ) ;
#3883=ORIENTED_EDGE ( 'NONE', *, *, #3766, .F. ) ;
#3909=AXIS2_PLACEMENT_3D ( 'NONE', #22133, #4125, #18483 ) ;
#3967=DIRECTION ( 'NONE',  ( -1.000000000000000000, -3.254448077276381206E-32, -1.066788928082016908E-26 ) ) ;
#3972=CARTESIAN_POINT ( 'NONE',  ( 24.75000000000001066, 2.000000000000099032, -16.99999999999999289 ) ) ;
#3974=DIRECTION ( 'NONE',  ( -1.066788928082016908E-26, 6.656013887802287108E-31, 1.000000000000000000 ) ) ;
#4005=LINE ( 'NONE', #16472, #20690 ) ;
#4038=CIRCLE ( 'NONE', #13062, 2.500000000000003553 ) ;
#4076=VECTOR ( 'NONE', #223, 1000.000000000000000 ) ;
#4110=COLOUR_RGB ( '', 0.31764706, 0.68627451, 0.89019608) ;
#4119=CARTESIAN_POINT ( 'NONE',  ( 2.499999999999988454, 4.500000000000059508, -3.469446951953614189E-14 ) ) ;
#4125=DIRECTION ( 'NONE',  ( -1.000000000000000000, -3.254448077276381206E-32, -1.066788928082016908E-26 ) ) ;
#4136=ORIENTED_EDGE ( 'NONE', *, *, #14675, .F. ) ;
#4159=CARTESIAN_POINT ( 'NONE',  ( 12.49999999999995914, 2.775557561562891982E-14, -4.750000000000002665 ) ) ;
#4186=VECTOR ( 'NONE', #4295, 1000.000000000000000 ) ;
#4187=EDGE_CURVE ( 'NONE', #23027, #12123, #295, .T. ) ;
#4188=ORIENTED_EDGE ( 'NONE', *, *, #7013, .F. ) ;
#4194=AXIS2_PLACEMENT_3D ( 'NONE', #6625, #13802, #2986 ) ;
#4196=DIRECTION ( 'NONE',  ( 0.000000000000000000, 0.000000000000000000, 1.000000000000000000 ) ) ;
#4200=EDGE_CURVE ( 'NONE', #11578, #13324, #7430, .T. ) ;
#4227=DIRECTION ( 'NONE',  ( 1.066786462891689527E-26, 6.656013887802287108E-31, 1.000000000000000000 ) ) ;
#4238=DIRECTION ( 'NONE',  ( -1.066786462891689527E-26, -6.656013887802287108E-31, -1.000000000000000000 ) ) ;
#4262=EDGE_CURVE ( 'NONE', #9468, #19219, #9812, .T. ) ;
#4288=CIRCLE ( 'NONE', #2417, 0.7500000000000006661 ) ;
#4295=DIRECTION ( 'NONE',  ( -1.000000000000000000, -3.254448077276381206E-32, -1.066788928082016908E-26 ) ) ;
#4307=ORIENTED_EDGE ( 'NONE', *, *, #14528, .F. ) ;
#4308=ORIENTED_EDGE ( 'NONE', *, *, #11113, .F. ) ;
#4335=ORIENTED_EDGE ( 'NONE', *, *, #5254, .T. ) ;
#4341=FACE_OUTER_BOUND ( 'NONE', #7364, .T. ) ;
#4346=DIRECTION ( 'NONE',  ( 1.000000000000000000, 0.000000000000000000, 0.000000000000000000 ) ) ;
#4365=ORIENTED_EDGE ( 'NONE', *, *, #20832, .T. ) ;
#4380=DIRECTION ( 'NONE',  ( -1.000000000000000000, -3.254448077276381206E-32, -1.066788928082016908E-26 ) ) ;
#4385=CARTESIAN_POINT ( 'NONE',  ( 22.50000000000003908, 4.500000000000031974, -0.2499999999999967526 ) ) ;
#4391=ORIENTED_EDGE ( 'NONE', *, *, #14279, .T. ) ;
#4413=CARTESIAN_POINT ( 'NONE',  ( 2.499999999999992006, 2.000000000000001776, -3.469446951953614189E-14 ) ) ;
#4441=VECTOR ( 'NONE', #20804, 1000.000000000000000 ) ;
#4450=DIRECTION ( 'NONE',  ( 1.000000000000000000, 0.000000000000000000, 0.000000000000000000 ) ) ;
#4465=( GEOMETRIC_REPRESENTATION_CONTEXT ( 3 ) GLOBAL_UNCERTAINTY_ASSIGNED_CONTEXT ( ( #14758 ) ) GLOBAL_UNIT_ASSIGNED_CONTEXT ( ( #9214, #11204, #7341 ) ) REPRESENTATION_CONTEXT ( 'NONE', 'WORKASPACE' ) );
#4468=VERTEX_POINT ( 'NONE', #10735 ) ;
#4495=ORIENTED_EDGE ( 'NONE', *, *, #8640, .T. ) ;
#4496=CARTESIAN_POINT ( 'NONE',  ( -2.081668171172168513E-14, 1.250000000000001110, 0.000000000000000000 ) ) ;
#4535=CIRCLE ( 'NONE', #4914, 2.500000000000002220 ) ;
#4546=VERTEX_POINT ( 'NONE', #14501 ) ;
#4569=VERTEX_POINT ( 'NONE', #16584 ) ;
#4586=VECTOR ( 'NONE', #12021, 1000.000000000000000 ) ;
#4592=TOROIDAL_SURFACE ( 'NONE', #7611, 1.750000000000000000, 0.2500000000000000000 ) ;
#4605=ORIENTED_EDGE ( 'NONE', *, *, #5254, .F. ) ;
#4616=DIRECTION ( 'NONE',  ( 0.000000000000000000, 0.000000000000000000, 1.000000000000000000 ) ) ;
#4660=ADVANCED_FACE ( 'NONE', ( #19504 ), #20558, .F. ) ;
#4718=CARTESIAN_POINT ( 'NONE',  ( -1.387778780781445676E-14, 2.000000000000001776, -2.000000000000001776 ) ) ;
#4737=LINE ( 'NONE', #2741, #5038 ) ;
#4739=DIRECTION ( 'NONE',  ( -1.720845688168991849E-15, 1.000000000000000000, 6.656013887802284481E-31 ) ) ;
#4745=DIRECTION ( 'NONE',  ( -1.000000000000000000, -3.254448077276381206E-32, -1.066788928082016908E-26 ) ) ;
#4749=ADVANCED_FACE ( 'NONE', ( #14215 ), #10352, .T. ) ;
#4752=ORIENTED_EDGE ( 'NONE', *, *, #5353, .F. ) ;
#4782=ORIENTED_EDGE ( 'NONE', *, *, #10486, .T. ) ;
#4790=CARTESIAN_POINT ( 'NONE',  ( 24.75000000000001776, 1.250000000000001110, -17.00000000000001066 ) ) ;
#4812=CIRCLE ( 'NONE', #17975, 0.2500000000000002220 ) ;
#4814=ORIENTED_EDGE ( 'NONE', *, *, #7145, .F. ) ;
#4856=DIRECTION ( 'NONE',  ( -1.000000000000000000, 0.000000000000000000, -1.066742637285843118E-26 ) ) ;
#4857=DIRECTION ( 'NONE',  ( 0.000000000000000000, 0.000000000000000000, 1.000000000000000000 ) ) ;
#4882=AXIS2_PLACEMENT_3D ( 'NONE', #14493, #7664, #21678 ) ;
#4891=ORIENTED_EDGE ( 'NONE', *, *, #14528, .T. ) ;
#4904=DIRECTION ( 'NONE',  ( 1.066786462891689527E-26, 6.656013887802287108E-31, 1.000000000000000000 ) ) ;
#4914=AXIS2_PLACEMENT_3D ( 'NONE', #22369, #11296, #6251 ) ;
#4943=CARTESIAN_POINT ( 'NONE',  ( 0.000000000000000000, 0.000000000000000000, 0.000000000000000000 ) ) ;
#4969=AXIS2_PLACEMENT_3D ( 'NONE', #5855, #16642, #22074 ) ;
#4983=ORIENTED_EDGE ( 'NONE', *, *, #10486, .F. ) ;
#5003=AXIS2_PLACEMENT_3D ( 'NONE', #9407, #19986, #15030 ) ;
#5038=VECTOR ( 'NONE', #991, 1000.000000000000000 ) ;
#5039=DIRECTION ( 'NONE',  ( 1.000000000000000000, 0.000000000000000000, 1.066788928082016908E-26 ) ) ;
#5043=VECTOR ( 'NONE', #18396, 999.9999999999998863 ) ;
#5060=ORIENTED_EDGE ( 'NONE', *, *, #14675, .T. ) ;
#5069=ADVANCED_FACE ( 'NONE', ( #19121 ), #14759, .T. ) ;
#5076=AXIS2_PLACEMENT_3D ( 'NONE', #6164, #13563, #20866 ) ;
#5080=VERTEX_POINT ( 'NONE', #23010 ) ;
#5081=ORIENTED_EDGE ( 'NONE', *, *, #3067, .T. ) ;
#5120=LINE ( 'NONE', #17699, #6897 ) ;
#5143=CARTESIAN_POINT ( 'NONE',  ( 0.2499999999999932832, 2.775557561562891351E-14, -2.000000000000001776 ) ) ;
#5160=FACE_OUTER_BOUND ( 'NONE', #2059, .T. ) ;
#5164=AXIS2_PLACEMENT_3D ( 'NONE', #9873, #7989, #20238 ) ;
#5189=MANIFOLD_SOLID_BREP ( 'Chamfer2', #6192 ) ;
#5191=LINE ( 'NONE', #16344, #22862 ) ;
#5196=AXIS2_PLACEMENT_3D ( 'NONE', #5302, #8949, #1989 ) ;
#5238=EDGE_CURVE ( 'NONE', #1275, #21027, #18467, .T. ) ;
#5250=DIRECTION ( 'NONE',  ( 1.000000000000000000, 0.000000000000000000, 0.000000000000000000 ) ) ;
#5254=EDGE_CURVE ( 'NONE', #15251, #14991, #18405, .T. ) ;
#5274=CARTESIAN_POINT ( 'NONE',  ( 2.499999999999998668, 2.000000000000001776, -18.75000000000001066 ) ) ;
#5300=VECTOR ( 'NONE', #17641, 1000.000000000000000 ) ;
#5302=CARTESIAN_POINT ( 'NONE',  ( 2.499999999999992006, 4.250000000000003553, -1.250000000000028866 ) ) ;
#5306=DIRECTION ( 'NONE',  ( 1.000000000000000000, 0.000000000000000000, 0.000000000000000000 ) ) ;
#5333=TOROIDAL_SURFACE ( 'NONE', #1927, 1.750000000000000000, 0.2500000000000000000 ) ;
#5353=EDGE_CURVE ( 'NONE', #9565, #21352, #15784, .T. ) ;
#5357=EDGE_CURVE ( 'NONE', #6270, #1104, #2707, .T. ) ;
#5391=TOROIDAL_SURFACE ( 'NONE', #8812, 0.7500000000000000000, 0.2500000000000000000 ) ;
#5415=ADVANCED_FACE ( 'NONE', ( #15330 ), #15472, .F. ) ;
#5417=LINE ( 'NONE', #1527, #17510 ) ;
#5426=DIRECTION ( 'NONE',  ( 1.000000000000000000, 3.254448077276381206E-32, 1.066788928082016908E-26 ) ) ;
#5454=FACE_OUTER_BOUND ( 'NONE', #657, .T. ) ;
#5477=DIRECTION ( 'NONE',  ( 1.066786462891689527E-26, 6.656013887802287108E-31, 1.000000000000000000 ) ) ;
#5480=EDGE_CURVE ( 'NONE', #20423, #20045, #17349, .T. ) ;
#5514=CARTESIAN_POINT ( 'NONE',  ( 0.2500000000000140998, 1.250000000000015099, 0.000000000000000000 ) ) ;
#5518=ADVANCED_FACE ( 'NONE', ( #5454 ), #17746, .T. ) ;
#5525=CARTESIAN_POINT ( 'NONE',  ( 2.499999999999960476, 4.250000000000017764, -18.75000000000002132 ) ) ;
#5543=EDGE_CURVE ( 'NONE', #17281, #3485, #7671, .T. ) ;
#5566=CARTESIAN_POINT ( 'NONE',  ( 25.00000000000000355, 2.000000000000001776, -2.000000000000005329 ) ) ;
#5600=DIRECTION ( 'NONE',  ( 0.000000000000000000, -1.734723475976805517E-15, 1.000000000000000000 ) ) ;
#5612=VERTEX_POINT ( 'NONE', #7556 ) ;
#5638=DIRECTION ( 'NONE',  ( -1.066786462891689527E-26, -6.656013887802287108E-31, -1.000000000000000000 ) ) ;
#5646=ORIENTED_EDGE ( 'NONE', *, *, #21775, .F. ) ;
#5647=FACE_OUTER_BOUND ( 'NONE', #482, .T. ) ;
#5660=AXIS2_PLACEMENT_3D ( 'NONE', #5794, #20132, #21793 ) ;
#5717=ADVANCED_FACE ( 'NONE', ( #968 ), #20232, .T. ) ;
#5742=DIRECTION ( 'NONE',  ( 1.000000000000000000, 3.254448077276381206E-32, 1.066788928082016908E-26 ) ) ;
#5749=DIRECTION ( 'NONE',  ( 0.000000000000000000, 0.000000000000000000, 1.000000000000000000 ) ) ;
#5755=DIRECTION ( 'NONE',  ( 1.000000000000000000, 3.254448077276381206E-32, 1.066788928082016908E-26 ) ) ;
#5757=AXIS2_PLACEMENT_3D ( 'NONE', #15694, #22893, #3370 ) ;
#5779=AXIS2_PLACEMENT_3D ( 'NONE', #11638, #16924, #2700 ) ;
#5794=CARTESIAN_POINT ( 'NONE',  ( 22.49999999999999645, 4.250000000000031974, -1.249999999999997558 ) ) ;
#5810=DIRECTION ( 'NONE',  ( 1.066786462891689527E-26, 6.656013887802287108E-31, 1.000000000000000000 ) ) ;
#5813=AXIS2_PLACEMENT_3D ( 'NONE', #6402, #1340, #8281 ) ;
#5816=ORIENTED_EDGE ( 'NONE', *, *, #15133, .T. ) ;
#5841=EDGE_CURVE ( 'NONE', #22552, #6184, #17599, .T. ) ;
#5855=CARTESIAN_POINT ( 'NONE',  ( 2.499999999999992006, 2.000000000000001776, -0.2500000000000349165 ) ) ;
#5914=SURFACE_SIDE_STYLE ('',( #22026 ) ) ;
#5915=ORIENTED_EDGE ( 'NONE', *, *, #7261, .T. ) ;
#5925=AXIS2_PLACEMENT_3D ( 'NONE', #7028, #17959, #22907 ) ;
#5940=CARTESIAN_POINT ( 'NONE',  ( 24.99999999999995737, 2.000000000000001776, -17.74999999999998224 ) ) ;
#5970=DIRECTION ( 'NONE',  ( 1.066786462891689527E-26, 6.656013887802287108E-31, 1.000000000000000000 ) ) ;
#6006=CARTESIAN_POINT ( 'NONE',  ( 24.75000000000001066, 2.000000000000099032, -16.99999999999997868 ) ) ;
#6072=ORIENTED_EDGE ( 'NONE', *, *, #15415, .T. ) ;
#6097=DIRECTION ( 'NONE',  ( -1.066786462891689527E-26, -6.656013887802287108E-31, -1.000000000000000000 ) ) ;
#6144=EDGE_CURVE ( 'NONE', #14991, #13234, #12077, .T. ) ;
#6154=ORIENTED_EDGE ( 'NONE', *, *, #14240, .F. ) ;
#6156=AXIS2_PLACEMENT_3D ( 'NONE', #2783, #10183, #2662 ) ;
#6164=CARTESIAN_POINT ( 'NONE',  ( 22.49999999999999645, 4.250000000000031974, -0.2500000000000036637 ) ) ;
#6184=VERTEX_POINT ( 'NONE', #823 ) ;
#6192=CLOSED_SHELL ( 'NONE', ( #4660, #5415, #6491, #366, #21160, #20826, #7374, #23230, #14266, #2167, #11114, #22694, #9274, #19167, #3234, #7383, #13121, #20861, #9538, #15105, #6255, #2892, #20039, #5717, #4749, #2527, #13134, #15705, #14906, #18451, #15388, #12568, #8902, #10569, #5518, #5069, #7425, #22943, #6472, #11519, #15651, #7686, #19478, #16565, #18269, #8217, #20272, #11911 ) ) ;
#6209=DIRECTION ( 'NONE',  ( -1.066786462891689527E-26, -6.656013887802287108E-31, -1.000000000000000000 ) ) ;
#6212=ORIENTED_EDGE ( 'NONE', *, *, #14276, .T. ) ;
#6226=DIRECTION ( 'NONE',  ( 0.000000000000000000, 1.297468594113506001E-30, 1.000000000000000000 ) ) ;
#6249=CARTESIAN_POINT ( 'NONE',  ( 22.49999999999998934, 4.250000000000017764, -18.75000000000001421 ) ) ;
#6251=DIRECTION ( 'NONE',  ( 1.000000000000000000, 0.000000000000000000, 0.000000000000000000 ) ) ;
#6255=ADVANCED_FACE ( 'NONE', ( #12320 ), #21520, .T. ) ;
#6270=VERTEX_POINT ( 'NONE', #19858 ) ;
#6274=DIRECTION ( 'NONE',  ( 8.659560561600564896E-17, 0.7071067811865516806, -0.7071067811865434649 ) ) ;
#6284=CARTESIAN_POINT ( 'NONE',  ( 2.499999999999998668, 2.000000000000001776, -17.75000000000000711 ) ) ;
#6302=EDGE_LOOP ( 'NONE', ( #18245, #10546, #14965, #5915 ) ) ;
#6307=AXIS2_PLACEMENT_3D ( 'NONE', #1120, #17445, #6628 ) ;
#6324=DIRECTION ( 'NONE',  ( -1.066811114794976679E-26, 0.000000000000000000, -1.000000000000000000 ) ) ;
#6329=EDGE_LOOP ( 'NONE', ( #6154, #13091, #13199, #15336 ) ) ;
#6402=CARTESIAN_POINT ( 'NONE',  ( 0.2500000000000036637, 2.000000000000001776, -17.00000000000000711 ) ) ;
#6417=ORIENTED_EDGE ( 'NONE', *, *, #6455, .T. ) ;
#6455=EDGE_CURVE ( 'NONE', #20477, #22552, #879, .T. ) ;
#6456=LINE ( 'NONE', #9872, #14092 ) ;
#6470=AXIS2_PLACEMENT_3D ( 'NONE', #14542, #8068, #11704 ) ;
#6472=ADVANCED_FACE ( 'NONE', ( #9155 ), #16407, .T. ) ;
#6489=DIRECTION ( 'NONE',  ( -1.066788928082016908E-26, 6.656013887802287108E-31, 1.000000000000000000 ) ) ;
#6491=ADVANCED_FACE ( 'NONE', ( #19211 ), #12145, .F. ) ;
#6503=EDGE_CURVE ( 'NONE', #8523, #14991, #18685, .T. ) ;
#6510=AXIS2_PLACEMENT_3D ( 'NONE', #8467, #6943, #21289 ) ;
#6519=DIRECTION ( 'NONE',  ( 1.066786462891689527E-26, 6.656013887802287108E-31, 1.000000000000000000 ) ) ;
#6558=EDGE_CURVE ( 'NONE', #21116, #21352, #15306, .T. ) ;
#6573=DIRECTION ( 'NONE',  ( 3.254448077146059901E-32, 1.000000000000000000, 6.409494854920712161E-31 ) ) ;
#6620=CARTESIAN_POINT ( 'NONE',  ( 25.00000000000001776, 1.250000000000028866, -2.081668171172168513E-14 ) ) ;
#6625=CARTESIAN_POINT ( 'NONE',  ( 12.49999999999992362, 1.250000000000015099, -9.500000000000001776 ) ) ;
#6628=DIRECTION ( 'NONE',  ( 0.000000000000000000, 1.297468594113506001E-30, 1.000000000000000000 ) ) ;
#6640=ORIENTED_EDGE ( 'NONE', *, *, #11484, .T. ) ;
#6693=CARTESIAN_POINT ( 'NONE',  ( 24.74999999999997513, 0.000000000000000000, -2.081668171172168513E-14 ) ) ;
#6726=ORIENTED_EDGE ( 'NONE', *, *, #4262, .F. ) ;
#6770=CARTESIAN_POINT ( 'NONE',  ( 22.49999999999996092, 2.000000000000043521, -17.75000000000001066 ) ) ;
#6773=VECTOR ( 'NONE', #4227, 1000.000000000000000 ) ;
#6816=DIRECTION ( 'NONE',  ( -1.066723072283233324E-26, 0.000000000000000000, -1.000000000000000000 ) ) ;
#6846=ORIENTED_EDGE ( 'NONE', *, *, #5480, .F. ) ;
#6869=PRODUCT ( 'Bracket washer', 'Bracket washer', '', ( #14252 ) ) ;
#6881=AXIS2_PLACEMENT_3D ( 'NONE', #6284, #14980, #9696 ) ;
#6897=VECTOR ( 'NONE', #20697, 999.9999999999998863 ) ;
#6912=ORIENTED_EDGE ( 'NONE', *, *, #20155, .T. ) ;
#6934=LINE ( 'NONE', #16081, #4076 ) ;
#6943=DIRECTION ( 'NONE',  ( -3.254448077146059901E-32, -1.000000000000000000, -6.409494854920712161E-31 ) ) ;
#7001=ORIENTED_EDGE ( 'NONE', *, *, #1615, .T. ) ;
#7013=EDGE_CURVE ( 'NONE', #1275, #10194, #5191, .T. ) ;
#7028=CARTESIAN_POINT ( 'NONE',  ( 1.040834085586084257E-14, 4.500000000000003553, 0.000000000000000000 ) ) ;
#7042=CARTESIAN_POINT ( 'NONE',  ( 0.2499999999999828748, 1.999999999999974021, -18.75000000000001066 ) ) ;
#7050=DIRECTION ( 'NONE',  ( 1.000000000000000000, 0.000000000000000000, 1.066194817212772764E-26 ) ) ;
#7058=AXIS2_PLACEMENT_3D ( 'NONE', #11389, #12935, #4450 ) ;
#7069=ORIENTED_EDGE ( 'NONE', *, *, #16810, .F. ) ;
#7125=VERTEX_POINT ( 'NONE', #9527 ) ;
#7131=ORIENTED_EDGE ( 'NONE', *, *, #9989, .F. ) ;
#7145=EDGE_CURVE ( 'NONE', #10170, #3062, #20980, .T. ) ;
#7146=DIRECTION ( 'NONE',  ( 0.000000000000000000, -6.162975822039153854E-31, -1.000000000000000000 ) ) ;
#7151=ORIENTED_EDGE ( 'NONE', *, *, #8666, .T. ) ;
#7153=( GEOMETRIC_REPRESENTATION_CONTEXT ( 3 ) GLOBAL_UNCERTAINTY_ASSIGNED_CONTEXT ( ( #16623 ) ) GLOBAL_UNIT_ASSIGNED_CONTEXT ( ( #16715, #22143, #20621 ) ) REPRESENTATION_CONTEXT ( 'NONE', 'WORKASPACE' ) );
#7194=EDGE_LOOP ( 'NONE', ( #16113, #11213, #15917, #7458 ) ) ;
#7230=VERTEX_POINT ( 'NONE', #17150 ) ;
#7237=CIRCLE ( 'NONE', #1942, 2.500000000000003997 ) ;
#7261=EDGE_CURVE ( 'NONE', #13207, #1275, #17596, .T. ) ;
#7278=CIRCLE ( 'NONE', #15129, 0.2500000000000000000 ) ;
#7293=DIRECTION ( 'NONE',  ( 1.000000000000000000, 3.254448077276381206E-32, 1.066788928082016908E-26 ) ) ;
#7297=CARTESIAN_POINT ( 'NONE',  ( 2.499999999999992006, 4.250000000000003553, -3.469446951953614189E-14 ) ) ;
#7341=( NAMED_UNIT ( * ) SI_UNIT ( $, .STERADIAN. ) SOLID_ANGLE_UNIT ( ) );
#7347=ORIENTED_EDGE ( 'NONE', *, *, #11113, .T. ) ;
#7351=LINE ( 'NONE', #68, #5043 ) ;
#7364=EDGE_LOOP ( 'NONE', ( #15684, #11575, #13126, #11930 ) ) ;
#7374=ADVANCED_FACE ( 'NONE', ( #5160 ), #18094, .F. ) ;
#7383=ADVANCED_FACE ( 'NONE', ( #12439 ), #1963, .F. ) ;
#7394=EDGE_CURVE ( 'NONE', #10194, #6184, #2960, .T. ) ;
#7395=EDGE_CURVE ( 'NONE', #9105, #10170, #6934, .T. ) ;
#7414=DIRECTION ( 'NONE',  ( 1.000000000000000000, 3.254448077276381206E-32, 1.066788928082016908E-26 ) ) ;
#7425=ADVANCED_FACE ( 'NONE', ( #109 ), #23172, .T. ) ;
#7430=CIRCLE ( 'NONE', #10065, 2.250000000000001776 ) ;
#7458=ORIENTED_EDGE ( 'NONE', *, *, #16140, .F. ) ;
#7498=LINE ( 'NONE', #18319, #2160 ) ;
#7514=VERTEX_POINT ( 'NONE', #9735 ) ;
#7542=FACE_OUTER_BOUND ( 'NONE', #7194, .T. ) ;
#7554=CARTESIAN_POINT ( 'NONE',  ( -2.081668171172168513E-14, 4.250000000000003553, -1.250000000000001110 ) ) ;
#7555=FACE_OUTER_BOUND ( 'NONE', #3387, .T. ) ;
#7556=CARTESIAN_POINT ( 'NONE',  ( 22.49999999999994671, 4.500000000000059508, -18.74999999999998224 ) ) ;
#7557=DIRECTION ( 'NONE',  ( 1.066786462891689527E-26, 6.656013887802287108E-31, 1.000000000000000000 ) ) ;
#7583=AXIS2_PLACEMENT_3D ( 'NONE', #4413, #7840, #15007 ) ;
#7610=STYLED_ITEM ( 'NONE', ( #12761 ), #5189 ) ;
#7611=AXIS2_PLACEMENT_3D ( 'NONE', #12400, #1819, #19582 ) ;
#7625=AXIS2_PLACEMENT_3D ( 'NONE', #6770, #19357, #20793 ) ;
#7629=PLANE ( 'NONE',  #8780 ) ;
#7639=LINE ( 'NONE', #18456, #19332 ) ;
#7649=EDGE_CURVE ( 'NONE', #8523, #16088, #15130, .T. ) ;
#7653=ORIENTED_EDGE ( 'NONE', *, *, #5357, .T. ) ;
#7664=DIRECTION ( 'NONE',  ( -3.254448077146059901E-32, -1.000000000000000000, 6.656013887802287108E-31 ) ) ;
#7671=LINE ( 'NONE', #12965, #9877 ) ;
#7685=UNCERTAINTY_MEASURE_WITH_UNIT (LENGTH_MEASURE( 1.000000000000000082E-05 ), #3474, 'distance_accuracy_value', 'NONE');
#7686=ADVANCED_FACE ( 'NONE', ( #10082 ), #20911, .T. ) ;
#7714=ORIENTED_EDGE ( 'NONE', *, *, #19578, .T. ) ;
#7731=VECTOR ( 'NONE', #14144, 1000.000000000000000 ) ;
#7738=DIRECTION ( 'NONE',  ( -1.066788928082016908E-26, -3.471809175856251779E-58, 1.000000000000000000 ) ) ;
#7764=CARTESIAN_POINT ( 'NONE',  ( 2.499999999999992006, 2.000000000000001776, -1.250000000000028866 ) ) ;
#7769=DIRECTION ( 'NONE',  ( 0.000000000000000000, 0.000000000000000000, -1.000000000000000000 ) ) ;
#7813=FACE_OUTER_BOUND ( 'NONE', #17928, .T. ) ;
#7817=DIRECTION ( 'NONE',  ( 1.000000000000000000, 3.254448077276381206E-32, 1.066788928082016908E-26 ) ) ;
#7840=DIRECTION ( 'NONE',  ( -1.066786462891689527E-26, -6.656013887802287108E-31, -1.000000000000000000 ) ) ;
#7857=ORIENTED_EDGE ( 'NONE', *, *, #6558, .F. ) ;
#7861=ORIENTED_EDGE ( 'NONE', *, *, #21596, .F. ) ;
#7887=PLANE ( 'NONE',  #15599 ) ;
#7899=PLANE ( 'NONE',  #20344 ) ;
#7924=CARTESIAN_POINT ( 'NONE',  ( 24.75000000000000355, 2.000000000000029310, -3.469446951953614189E-15 ) ) ;
#7941=VERTEX_POINT ( 'NONE', #18411 ) ;
#7949=DIRECTION ( 'NONE',  ( -1.066786462891689527E-26, -6.656013887802287108E-31, -1.000000000000000000 ) ) ;
#7960=EDGE_CURVE ( 'NONE', #5080, #8523, #8992, .T. ) ;
#7971=ORIENTED_EDGE ( 'NONE', *, *, #14279, .F. ) ;
#7981=VECTOR ( 'NONE', #17229, 1000.000000000000000 ) ;
#7984=CIRCLE ( 'NONE', #18125, 0.2500000000000002220 ) ;
#7989=DIRECTION ( 'NONE',  ( 1.000000000000000000, 3.254448077276381206E-32, 1.066788928082016908E-26 ) ) ;
#8007=CARTESIAN_POINT ( 'NONE',  ( 22.49999999999998224, 2.000000000000001776, -2.081668171172168513E-14 ) ) ;
#8068=DIRECTION ( 'NONE',  ( -1.066786462891689527E-26, -6.656013887802287108E-31, -1.000000000000000000 ) ) ;
#8085=ORIENTED_EDGE ( 'NONE', *, *, #21191, .T. ) ;
#8096=EDGE_CURVE ( 'NONE', #3485, #7125, #449, .T. ) ;
#8115=ORIENTED_EDGE ( 'NONE', *, *, #21629, .F. ) ;
#8121=DIRECTION ( 'NONE',  ( 1.066786462891689527E-26, 6.656013887802287108E-31, 1.000000000000000000 ) ) ;
#8128=DIRECTION ( 'NONE',  ( -3.254448077146059901E-32, -1.000000000000000000, -6.409494854920712161E-31 ) ) ;
#8142=VECTOR ( 'NONE', #14421, 1000.000000000000000 ) ;
#8178=AXIS2_PLACEMENT_3D ( 'NONE', #21991, #16672, #6226 ) ;
#8204=ORIENTED_EDGE ( 'NONE', *, *, #4200, .F. ) ;
#8211=CARTESIAN_POINT ( 'NONE',  ( 24.75000000000000355, 2.000000000000029310, -2.000000000000005329 ) ) ;
#8217=ADVANCED_FACE ( 'NONE', ( #10090 ), #9494, .T. ) ;
#8218=CARTESIAN_POINT ( 'NONE',  ( 22.49999999999996092, 2.000000000000043521, -17.75000000000001066 ) ) ;
#8266=ORIENTED_EDGE ( 'NONE', *, *, #5543, .T. ) ;
#8268=EDGE_LOOP ( 'NONE', ( #2473, #18537, #4188, #9124 ) ) ;
#8281=DIRECTION ( 'NONE',  ( 1.066788928082016908E-26, 3.471809175856251779E-58, -1.000000000000000000 ) ) ;
#8328=CARTESIAN_POINT ( 'NONE',  ( 0.2499999999999828748, 1.999999999999974021, -19.00000000000001066 ) ) ;
#8329=DIRECTION ( 'NONE',  ( -1.066786462891689527E-26, -6.656013887802287108E-31, -1.000000000000000000 ) ) ;
#8338=FACE_OUTER_BOUND ( 'NONE', #21444, .T. ) ;
#8401=CARTESIAN_POINT ( 'NONE',  ( 24.75000000000001066, 2.000000000000099032, -17.49999999999998224 ) ) ;
#8402=DIRECTION ( 'NONE',  ( 0.000000000000000000, 0.000000000000000000, -1.000000000000000000 ) ) ;
#8404=DIRECTION ( 'NONE',  ( -1.066786462891689527E-26, -6.656013887802287108E-31, -1.000000000000000000 ) ) ;
#8463=DIRECTION ( 'NONE',  ( 1.000000000000000000, -3.739292825994448183E-14, 0.000000000000000000 ) ) ;
#8467=CARTESIAN_POINT ( 'NONE',  ( 12.49999999999995914, 2.775557561562891351E-14, -9.500000000000003553 ) ) ;
#8478=DIRECTION ( 'NONE',  ( 1.000000000000000000, 3.254448077276381206E-32, 1.066788928082016908E-26 ) ) ;
#8523=VERTEX_POINT ( 'NONE', #13096 ) ;
#8608=EDGE_LOOP ( 'NONE', ( #7347, #7069, #19366, #22965 ) ) ;
#8629=ORIENTED_EDGE ( 'NONE', *, *, #20925, .F. ) ;
#8638=APPLICATION_CONTEXT ( 'automotive_design' ) ;
#8640=EDGE_CURVE ( 'NONE', #20161, #23027, #18847, .T. ) ;
#8666=EDGE_CURVE ( 'NONE', #20884, #10194, #7278, .T. ) ;
#8724=EDGE_LOOP ( 'NONE', ( #14166, #11868, #114, #16485 ) ) ;
#8725=ORIENTED_EDGE ( 'NONE', *, *, #12220, .T. ) ;
#8741=CIRCLE ( 'NONE', #3104, 1.749999999999999778 ) ;
#8744=CARTESIAN_POINT ( 'NONE',  ( 12.49999999999992362, 1.250000000000015099, -9.500000000000001776 ) ) ;
#8769=DIRECTION ( 'NONE',  ( -1.000000000000000000, -1.734723475976804728E-15, 0.000000000000000000 ) ) ;
#8775=DIRECTION ( 'NONE',  ( 1.000000000000000000, 3.254448077276381206E-32, 1.066788928082016908E-26 ) ) ;
#8780=AXIS2_PLACEMENT_3D ( 'NONE', #346, #3974, #15024 ) ;
#8789=ORIENTED_EDGE ( 'NONE', *, *, #17570, .T. ) ;
#8811=DIRECTION ( 'NONE',  ( -1.066786462891689527E-26, -6.656013887802287108E-31, -1.000000000000000000 ) ) ;
#8812=AXIS2_PLACEMENT_3D ( 'NONE', #23082, #8948, #12345 ) ;
#8866=DIRECTION ( 'NONE',  ( 0.000000000000000000, 0.000000000000000000, -1.000000000000000000 ) ) ;
#8877=CYLINDRICAL_SURFACE ( 'NONE', #12940, 0.2500000000000002220 ) ;
#8892=DIRECTION ( 'NONE',  ( 0.000000000000000000, 0.000000000000000000, -1.000000000000000000 ) ) ;
#8902=ADVANCED_FACE ( 'NONE', ( #7542 ), #21912, .T. ) ;
#8919=AXIS2_PLACEMENT_3D ( 'NONE', #15182, #14720, #22377 ) ;
#8921=CARTESIAN_POINT ( 'NONE',  ( 24.75000000000001776, 0.2500000000000418554, -2.081668171172168513E-14 ) ) ;
#8933=EDGE_LOOP ( 'NONE', ( #4752, #8725, #2186, #2031 ) ) ;
#8948=DIRECTION ( 'NONE',  ( -1.000000000000000000, -3.254448077276381206E-32, -1.066788928082016908E-26 ) ) ;
#8949=DIRECTION ( 'NONE',  ( -1.000000000000000000, -3.254448077276381206E-32, -1.066788928082016908E-26 ) ) ;
#8951=CIRCLE ( 'NONE', #13832, 2.250000000000001776 ) ;
#8970=LINE ( 'NONE', #17795, #7731 ) ;
#8974=CARTESIAN_POINT ( 'NONE',  ( 22.49999999999992539, 1.999999999999960032, -19.00000000000001421 ) ) ;
#8992=CIRCLE ( 'NONE', #16864, 2.250000000000001776 ) ;
#9018=STYLED_ITEM ( 'NONE', ( #2376 ), #15637 ) ;
#9068=EDGE_LOOP ( 'NONE', ( #13125, #627, #15650, #3007 ) ) ;
#9089=AXIS2_PLACEMENT_3D ( 'NONE', #9276, #6097, #18100 ) ;
#9105=VERTEX_POINT ( 'NONE', #1183 ) ;
#9124=ORIENTED_EDGE ( 'NONE', *, *, #13555, .T. ) ;
#9144=DIRECTION ( 'NONE',  ( 0.000000000000000000, 0.000000000000000000, -1.000000000000000000 ) ) ;
#9155=FACE_OUTER_BOUND ( 'NONE', #14625, .T. ) ;
#9158=DIRECTION ( 'NONE',  ( 1.000000000000000000, 0.000000000000000000, 0.000000000000000000 ) ) ;
#9188=EDGE_LOOP ( 'NONE', ( #17158, #6640, #8266, #18048 ) ) ;
#9193=VECTOR ( 'NONE', #6274, 999.9999999999998863 ) ;
#9214=( LENGTH_UNIT ( ) NAMED_UNIT ( * ) SI_UNIT ( .MILLI., .METRE. ) );
#9219=EDGE_LOOP ( 'NONE', ( #14535, #3150 ) ) ;
#9245=ORIENTED_EDGE ( 'NONE', *, *, #12707, .F. ) ;
#9274=ADVANCED_FACE ( 'NONE', ( #696 ), #7629, .F. ) ;
#9276=CARTESIAN_POINT ( 'NONE',  ( 0.2499999999999724665, 0.2500000000000140998, 0.000000000000000000 ) ) ;
#9277=ORIENTED_EDGE ( 'NONE', *, *, #19319, .F. ) ;
#9333=AXIS2_PLACEMENT_3D ( 'NONE', #11426, #6489, #20856 ) ;
#9342=AXIS2_PLACEMENT_3D ( 'NONE', #21411, #17624, #3732 ) ;
#9365=ORIENTED_EDGE ( 'NONE', *, *, #14163, .T. ) ;
#9386=EDGE_CURVE ( 'NONE', #4546, #2242, #21570, .T. ) ;
#9391=EDGE_CURVE ( 'NONE', #20161, #21498, #1281, .T. ) ;
#9393=ORIENTED_EDGE ( 'NONE', *, *, #7649, .T. ) ;
#9407=CARTESIAN_POINT ( 'NONE',  ( 24.75000000000001066, 2.000000000000099032, -16.99999999999997868 ) ) ;
#9468=VERTEX_POINT ( 'NONE', #9750 ) ;
#9477=EDGE_CURVE ( 'NONE', #21352, #21116, #10612, .T. ) ;
#9494=TOROIDAL_SURFACE ( 'NONE', #11362, 1.750000000000000000, 0.2500000000000000000 ) ;
#9497=ORIENTED_EDGE ( 'NONE', *, *, #20189, .T. ) ;
#9498=EDGE_CURVE ( 'NONE', #10170, #10973, #7984, .T. ) ;
#9499=ORIENTED_EDGE ( 'NONE', *, *, #9835, .T. ) ;
#9512=DIRECTION ( 'NONE',  ( 0.000000000000000000, 0.000000000000000000, 1.000000000000000000 ) ) ;
#9521=DIRECTION ( 'NONE',  ( -1.066786462891689527E-26, -6.656013887802287108E-31, -1.000000000000000000 ) ) ;
#9527=CARTESIAN_POINT ( 'NONE',  ( 22.49999999999996092, 4.500000000000073719, -17.74999999999998224 ) ) ;
#9538=ADVANCED_FACE ( 'NONE', ( #3035 ), #18802, .T. ) ;
#9554=DIRECTION ( 'NONE',  ( 1.066786462891689527E-26, 6.656013887802287108E-31, 1.000000000000000000 ) ) ;
#9565=VERTEX_POINT ( 'NONE', #22688 ) ;
#9606=AXIS2_PLACEMENT_3D ( 'NONE', #5274, #10447, #17053 ) ;
#9677=VERTEX_POINT ( 'NONE', #5143 ) ;
#9678=EDGE_LOOP ( 'NONE', ( #9852, #4307, #20517, #16604 ) ) ;
#9680=CIRCLE ( 'NONE', #18315, 2.000000000000001776 ) ;
#9696=DIRECTION ( 'NONE',  ( -1.000000000000000000, 7.100545512326564696E-57, 1.066786462891689527E-26 ) ) ;
#9699=DIRECTION ( 'NONE',  ( -1.066786462891689527E-26, -6.656013887802287108E-31, -1.000000000000000000 ) ) ;
#9700=CARTESIAN_POINT ( 'NONE',  ( 24.75000000000000355, 2.000000000000029310, -1.250000000000004663 ) ) ;
#9702=DIRECTION ( 'NONE',  ( 1.066788928082016908E-26, 3.471809175856251779E-58, -1.000000000000000000 ) ) ;
#9725=FACE_OUTER_BOUND ( 'NONE', #17422, .T. ) ;
#9735=CARTESIAN_POINT ( 'NONE',  ( 12.49999999999995914, 0.2500000000000002220, -4.750000000000002665 ) ) ;
#9750=CARTESIAN_POINT ( 'NONE',  ( 2.499999999999988454, 4.500000000000059508, -0.2500000000000349165 ) ) ;
#9757=FACE_OUTER_BOUND ( 'NONE', #18098, .T. ) ;
#9811=CARTESIAN_POINT ( 'NONE',  ( 24.74999999999994316, 6.938893903907228378E-14, -17.00000000000001066 ) ) ;
#9812=LINE ( 'NONE', #4385, #19825 ) ;
#9835=EDGE_CURVE ( 'NONE', #16088, #16004, #3102, .T. ) ;
#9842=DIRECTION ( 'NONE',  ( -3.254448077146059901E-32, -1.000000000000000000, -6.409494854920712161E-31 ) ) ;
#9852=ORIENTED_EDGE ( 'NONE', *, *, #9391, .T. ) ;
#9858=AXIS2_PLACEMENT_3D ( 'NONE', #5566, #10503, #10613 ) ;
#9867=AXIS2_PLACEMENT_3D ( 'NONE', #9982, #6573, #15375 ) ;
#9872=CARTESIAN_POINT ( 'NONE',  ( 2.499999999999981348, 4.250000000000087041, -17.50000000000001776 ) ) ;
#9873=CARTESIAN_POINT ( 'NONE',  ( -1.387778780781445676E-14, 2.000000000000001776, -2.000000000000001776 ) ) ;
#9876=LINE ( 'NONE', #17266, #17502 ) ;
#9877=VECTOR ( 'NONE', #9554, 1000.000000000000000 ) ;
#9898=AXIS2_PLACEMENT_3D ( 'NONE', #12876, #19715, #5600 ) ;
#9971=CARTESIAN_POINT ( 'NONE',  ( 2.499999999999981348, 4.250000000000087041, -17.75000000000001776 ) ) ;
#9982=CARTESIAN_POINT ( 'NONE',  ( 12.49999999999992362, 1.250000000000015099, -9.500000000000001776 ) ) ;
#9989=EDGE_CURVE ( 'NONE', #9677, #2242, #14378, .T. ) ;
#10024=ORIENTED_EDGE ( 'NONE', *, *, #16690, .F. ) ;
#10065=AXIS2_PLACEMENT_3D ( 'NONE', #11912, #6519, #4856 ) ;
#10068=DIRECTION ( 'NONE',  ( 1.066788928082016908E-26, -6.656013887802287108E-31, -1.000000000000000000 ) ) ;
#10082=FACE_OUTER_BOUND ( 'NONE', #22793, .T. ) ;
#10084=DIRECTION ( 'NONE',  ( 0.000000000000000000, 0.000000000000000000, 1.000000000000000000 ) ) ;
#10090=FACE_OUTER_BOUND ( 'NONE', #21670, .T. ) ;
#10109=CARTESIAN_POINT ( 'NONE',  ( -6.938893903907228378E-15, 1.500000000000001332, 0.000000000000000000 ) ) ;
#10137=DIRECTION ( 'NONE',  ( -1.000000000000000000, -3.254448077276381206E-32, -1.066788928082016908E-26 ) ) ;
#10138=PRODUCT_DEFINITION_FORMATION_WITH_SPECIFIED_SOURCE ( 'ANY', '', #6869, .NOT_KNOWN. ) ;
#10163=ORIENTED_EDGE ( 'NONE', *, *, #4200, .T. ) ;
#10170=VERTEX_POINT ( 'NONE', #12869 ) ;
#10183=DIRECTION ( 'NONE',  ( 3.254448077146059901E-32, 1.000000000000000000, -6.656013887802287108E-31 ) ) ;
#10194=VERTEX_POINT ( 'NONE', #20053 ) ;
#10206=AXIS2_PLACEMENT_3D ( 'NONE', #7554, #12841, #16702 ) ;
#10267=CARTESIAN_POINT ( 'NONE',  ( 24.75000000000000355, 2.000000000000029310, -3.469446951953614189E-15 ) ) ;
#10283=ORIENTED_EDGE ( 'NONE', *, *, #924, .T. ) ;
#10336=CARTESIAN_POINT ( 'NONE',  ( -1.734723475976807094E-14, 2.000000000000001776, -17.00000000000000711 ) ) ;
#10352=TOROIDAL_SURFACE ( 'NONE', #9606, 2.250000000000000444, 0.2500000000000000000 ) ;
#10406=AXIS2_PLACEMENT_3D ( 'NONE', #18830, #8128, #12194 ) ;
#10413=FACE_OUTER_BOUND ( 'NONE', #21357, .T. ) ;
#10444=CIRCLE ( 'NONE', #3296, 2.000000000000000000 ) ;
#10447=DIRECTION ( 'NONE',  ( 1.066786462891689527E-26, 6.656013887802287108E-31, 1.000000000000000000 ) ) ;
#10454=DIRECTION ( 'NONE',  ( -1.000000000000000000, -3.254448077276381206E-32, -1.066788928082016908E-26 ) ) ;
#10482=VERTEX_POINT ( 'NONE', #3535 ) ;
#10486=EDGE_CURVE ( 'NONE', #19482, #21027, #23057, .T. ) ;
#10499=CARTESIAN_POINT ( 'NONE',  ( 24.99999999999995737, 2.000000000000001776, -16.99999999999997868 ) ) ;
#10503=DIRECTION ( 'NONE',  ( -1.000000000000000000, -3.254448077276381206E-32, -1.066788928082016908E-26 ) ) ;
#10521=FACE_OUTER_BOUND ( 'NONE', #8608, .T. ) ;
#10546=ORIENTED_EDGE ( 'NONE', *, *, #7394, .T. ) ;
#10554=CARTESIAN_POINT ( 'NONE',  ( 2.499999999999960476, 4.250000000000017764, -19.00000000000002132 ) ) ;
#10569=ADVANCED_FACE ( 'NONE', ( #5647 ), #21566, .T. ) ;
#10607=DIRECTION ( 'NONE',  ( 1.000000000000000000, -3.816391647148972452E-14, 0.000000000000000000 ) ) ;
#10612=CIRCLE ( 'NONE', #9867, 4.750000000000000888 ) ;
#10613=DIRECTION ( 'NONE',  ( 0.000000000000000000, 0.000000000000000000, 1.000000000000000000 ) ) ;
#10643=FILL_AREA_STYLE_COLOUR ( '', #20393 ) ;
#10664=DIRECTION ( 'NONE',  ( -3.254448077146059901E-32, -1.000000000000000000, -6.409494854920712161E-31 ) ) ;
#10716=ORIENTED_EDGE ( 'NONE', *, *, #22905, .F. ) ;
#10735=CARTESIAN_POINT ( 'NONE',  ( 24.99999999999996447, 1.999999999999988010, -18.74999999999998224 ) ) ;
#10744=ORIENTED_EDGE ( 'NONE', *, *, #17685, .T. ) ;
#10759=( NAMED_UNIT ( * ) PLANE_ANGLE_UNIT ( ) SI_UNIT ( $, .RADIAN. ) );
#10766=EDGE_LOOP ( 'NONE', ( #23071, #13590, #21419, #14855 ) ) ;
#10792=EDGE_CURVE ( 'NONE', #7125, #17822, #20434, .T. ) ;
#10794=VECTOR ( 'NONE', #11973, 1000.000000000000000 ) ;
#10801=CIRCLE ( 'NONE', #282, 0.2500000000000002220 ) ;
#10841=DIRECTION ( 'NONE',  ( -3.254448077146059901E-32, -1.000000000000000000, -6.409494854920712161E-31 ) ) ;
#10849=DIRECTION ( 'NONE',  ( 1.000000000000000000, 3.254448077276381206E-32, 1.066788928082016908E-26 ) ) ;
#10865=ORIENTED_EDGE ( 'NONE', *, *, #6503, .F. ) ;
#10891=DIRECTION ( 'NONE',  ( 0.000000000000000000, 0.000000000000000000, 1.000000000000000000 ) ) ;
#10893=AXIS2_PLACEMENT_3D ( 'NONE', #12724, #14834, #13072 ) ;
#10908=FACE_OUTER_BOUND ( 'NONE', #21183, .T. ) ;
#10968=EDGE_CURVE ( 'NONE', #4546, #9468, #22631, .T. ) ;
#10973=VERTEX_POINT ( 'NONE', #22190 ) ;
#11070=EDGE_CURVE ( 'NONE', #4468, #3633, #8741, .T. ) ;
#11085=ORIENTED_EDGE ( 'NONE', *, *, #22498, .F. ) ;
#11113=EDGE_CURVE ( 'NONE', #9105, #19482, #20378, .T. ) ;
#11114=ADVANCED_FACE ( 'NONE', ( #19118 ), #13367, .F. ) ;
#11118=AXIS2_PLACEMENT_3D ( 'NONE', #5525, #11270, #4196 ) ;
#11162=FACE_OUTER_BOUND ( 'NONE', #8933, .T. ) ;
#11202=ORIENTED_EDGE ( 'NONE', *, *, #16810, .T. ) ;
#11204=( NAMED_UNIT ( * ) PLANE_ANGLE_UNIT ( ) SI_UNIT ( $, .RADIAN. ) );
#11212=ORIENTED_EDGE ( 'NONE', *, *, #11070, .T. ) ;
#11213=ORIENTED_EDGE ( 'NONE', *, *, #7394, .F. ) ;
#11248=DIRECTION ( 'NONE',  ( 1.066194817212773768E-26, 0.000000000000000000, 1.000000000000000000 ) ) ;
#11266=LINE ( 'NONE', #13158, #16209 ) ;
#11270=DIRECTION ( 'NONE',  ( -1.000000000000000000, -3.254448077276381206E-32, -1.066788928082016908E-26 ) ) ;
#11296=DIRECTION ( 'NONE',  ( 1.066786462891689527E-26, 6.656013887802287108E-31, 1.000000000000000000 ) ) ;
#11300=CARTESIAN_POINT ( 'NONE',  ( 2.499999999999998668, 2.000000000000001776, -17.50000000000000711 ) ) ;
#11309=AXIS2_PLACEMENT_3D ( 'NONE', #12070, #4904, #15837 ) ;
#11330=DIRECTION ( 'NONE',  ( 1.000000000000000000, 1.734723475976805517E-15, 0.000000000000000000 ) ) ;
#11348=EDGE_CURVE ( 'NONE', #11578, #20045, #17755, .T. ) ;
#11362=AXIS2_PLACEMENT_3D ( 'NONE', #8211, #13621, #11608 ) ;
#11389=CARTESIAN_POINT ( 'NONE',  ( 22.49999999999992539, 1.999999999999960032, -18.75000000000001421 ) ) ;
#11406=DIRECTION ( 'NONE',  ( 1.066786462891689527E-26, 6.656013887802287108E-31, 1.000000000000000000 ) ) ;
#11411=CIRCLE ( 'NONE', #13308, 0.5000000000000004441 ) ;
#11426=CARTESIAN_POINT ( 'NONE',  ( 3.469446951953614189E-15, 1.500000000000015099, -19.00000000000001066 ) ) ;
#11459=ORIENTED_EDGE ( 'NONE', *, *, #778, .T. ) ;
#11461=ORIENTED_EDGE ( 'NONE', *, *, #21191, .F. ) ;
#11472=CARTESIAN_POINT ( 'NONE',  ( -2.081668171172168513E-14, 4.250000000000003553, -0.2500000000000002220 ) ) ;
#11478=CARTESIAN_POINT ( 'NONE',  ( 0.2499999999999794054, 1.500000000000015099, -2.000000000000001776 ) ) ;
#11484=EDGE_CURVE ( 'NONE', #5612, #17281, #2742, .T. ) ;
#11499=ORIENTED_EDGE ( 'NONE', *, *, #23048, .F. ) ;
#11519=ADVANCED_FACE ( 'NONE', ( #7813 ), #15128, .T. ) ;
#11532=EDGE_CURVE ( 'NONE', #3062, #17822, #20027, .T. ) ;
#11541=AXIS2_PLACEMENT_3D ( 'NONE', #2515, #5742, #9702 ) ;
#11546=AXIS2_PLACEMENT_3D ( 'NONE', #2168, #8404, #11568 ) ;
#11568=DIRECTION ( 'NONE',  ( -1.000000000000000000, 0.000000000000000000, 0.000000000000000000 ) ) ;
#11572=AXIS2_PLACEMENT_3D ( 'NONE', #23200, #10137, #12001 ) ;
#11575=ORIENTED_EDGE ( 'NONE', *, *, #10968, .F. ) ;
#11578=VERTEX_POINT ( 'NONE', #10267 ) ;
#11586=CARTESIAN_POINT ( 'NONE',  ( 2.499999999999998668, 2.000000000000001776, -19.00000000000001066 ) ) ;
#11592=DIRECTION ( 'NONE',  ( -1.000000000000000000, 0.000000000000000000, -1.066879592304109953E-26 ) ) ;
#11608=DIRECTION ( 'NONE',  ( -1.066788928082016908E-26, -3.471809175856251779E-58, 1.000000000000000000 ) ) ;
#11636=DIRECTION ( 'NONE',  ( -1.000000000000000000, -3.254448077276381206E-32, 1.066786462891689527E-26 ) ) ;
#11638=CARTESIAN_POINT ( 'NONE',  ( 2.499999999999992006, 2.000000000000001776, -0.2500000000000349165 ) ) ;
#11661=ORIENTED_EDGE ( 'NONE', *, *, #17685, .F. ) ;
#11670=CARTESIAN_POINT ( 'NONE',  ( 24.75000000000000355, 2.000000000000029310, -1.500000000000004885 ) ) ;
#11675=DIRECTION ( 'NONE',  ( -1.000000000000000000, -3.254448077276381206E-32, -1.066788928082016908E-26 ) ) ;
#11704=DIRECTION ( 'NONE',  ( -1.000000000000000000, 0.000000000000000000, 0.000000000000000000 ) ) ;
#11749=CIRCLE ( 'NONE', #17773, 0.2500000000000002220 ) ;
#11754=AXIS2_PLACEMENT_3D ( 'NONE', #7764, #11406, #21788 ) ;
#11770=AXIS2_PLACEMENT_3D ( 'NONE', #17639, #21428, #12695 ) ;
#11772=AXIS2_PLACEMENT_3D ( 'NONE', #10336, #15744, #6816 ) ;
#11799=DIRECTION ( 'NONE',  ( 0.000000000000000000, -1.431146867680864591E-14, -1.000000000000000000 ) ) ;
#11802=CARTESIAN_POINT ( 'NONE',  ( 12.49999999999995914, 2.775557561562891036E-14, -14.25000000000000355 ) ) ;
#11868=ORIENTED_EDGE ( 'NONE', *, *, #17044, .T. ) ;
#11871=EDGE_CURVE ( 'NONE', #1774, #14364, #12906, .T. ) ;
#11897=EDGE_LOOP ( 'NONE', ( #7861, #15539, #17905, #11461 ) ) ;
#11907=DIRECTION ( 'NONE',  ( -1.000000000000000000, -1.734723475976805517E-15, 0.000000000000000000 ) ) ;
#11911=ADVANCED_FACE ( 'NONE', ( #1523 ), #21933, .F. ) ;
#11912=CARTESIAN_POINT ( 'NONE',  ( 22.49999999999998224, 2.000000000000001776, -2.081668171172168513E-14 ) ) ;
#11930=ORIENTED_EDGE ( 'NONE', *, *, #15118, .F. ) ;
#11964=AXIS2_PLACEMENT_3D ( 'NONE', #14099, #10454, #21639 ) ;
#11970=CARTESIAN_POINT ( 'NONE',  ( 2.499999999999998668, 4.500000000000031974, -17.75000000000001776 ) ) ;
#11973=DIRECTION ( 'NONE',  ( 1.066786462891689527E-26, 6.656013887802287108E-31, 1.000000000000000000 ) ) ;
#11982=ORIENTED_EDGE ( 'NONE', *, *, #2329, .T. ) ;
#12001=DIRECTION ( 'NONE',  ( 1.066194817212772764E-26, 0.000000000000000000, 1.000000000000000000 ) ) ;
#12010=EDGE_LOOP ( 'NONE', ( #20534, #4365, #17535, #11202, #4782, #17155, #6846, #11459 ) ) ;
#12021=DIRECTION ( 'NONE',  ( 3.254448077146059901E-32, 1.000000000000000000, 6.409494854920712161E-31 ) ) ;
#12026=APPLICATION_CONTEXT ( 'automotive_design' ) ;
#12070=CARTESIAN_POINT ( 'NONE',  ( 22.49999999999998224, 2.000000000000001776, -1.250000000000021982 ) ) ;
#12077=LINE ( 'NONE', #6693, #10794 ) ;
#12079=CARTESIAN_POINT ( 'NONE',  ( 22.49999999999998224, 2.000000000000001776, -1.500000000000022204 ) ) ;
#12082=AXIS2_PLACEMENT_3D ( 'NONE', #12732, #10849, #18148 ) ;
#12088=VECTOR ( 'NONE', #22339, 1000.000000000000000 ) ;
#12091=AXIS2_PLACEMENT_3D ( 'NONE', #20457, #1162, #2676 ) ;
#12123=VERTEX_POINT ( 'NONE', #15828 ) ;
#12145=CYLINDRICAL_SURFACE ( 'NONE', #6307, 4.750000000000000888 ) ;
#12193=FACE_OUTER_BOUND ( 'NONE', #6329, .T. ) ;
#12194=DIRECTION ( 'NONE',  ( 0.000000000000000000, -6.162975822039153854E-31, -1.000000000000000000 ) ) ;
#12196=CONICAL_SURFACE ( 'NONE', #21988, 4.750000000000000888, 0.7853981633974430610 ) ;
#12220=EDGE_CURVE ( 'NONE', #9565, #7514, #16647, .T. ) ;
#12320=FACE_OUTER_BOUND ( 'NONE', #8724, .T. ) ;
#12345=DIRECTION ( 'NONE',  ( -1.066788928082016908E-26, -3.471809175856251779E-58, 1.000000000000000000 ) ) ;
#12352=CYLINDRICAL_SURFACE ( 'NONE', #11572, 0.2500000000000002220 ) ;
#12383=ORIENTED_EDGE ( 'NONE', *, *, #9498, .T. ) ;
#12400=CARTESIAN_POINT ( 'NONE',  ( 0.2499999999999655276, 2.000000000000015543, -2.000000000000001776 ) ) ;
#12408=CIRCLE ( 'NONE', #2272, 0.2500000000000000000 ) ;
#12439=FACE_OUTER_BOUND ( 'NONE', #19575, .T. ) ;
#12461=FACE_OUTER_BOUND ( 'NONE', #9068, .T. ) ;
#12508=CIRCLE ( 'NONE', #2733, 0.2500000000000002220 ) ;
#12538=ORIENTED_EDGE ( 'NONE', *, *, #1742, .F. ) ;
#12568=ADVANCED_FACE ( 'NONE', ( #10521 ), #8877, .T. ) ;
#12604=FACE_OUTER_BOUND ( 'NONE', #2175, .T. ) ;
#12676=DIRECTION ( 'NONE',  ( 1.066786462891689527E-26, 6.656013887802287108E-31, 1.000000000000000000 ) ) ;
#12693=AXIS2_PLACEMENT_3D ( 'NONE', #8744, #15903, #23114 ) ;
#12695=DIRECTION ( 'NONE',  ( 0.000000000000000000, 0.000000000000000000, 1.000000000000000000 ) ) ;
#12707=EDGE_CURVE ( 'NONE', #7514, #1104, #7351, .T. ) ;
#12724=CARTESIAN_POINT ( 'NONE',  ( 2.499999999999998668, 2.000000000000001776, -18.75000000000001066 ) ) ;
#12732=CARTESIAN_POINT ( 'NONE',  ( 0.2499999999999655276, 2.000000000000015543, -2.000000000000001776 ) ) ;
#12761=PRESENTATION_STYLE_ASSIGNMENT (( #21488 ) ) ;
#12765=DIRECTION ( 'NONE',  ( 0.000000000000000000, 0.000000000000000000, -1.000000000000000000 ) ) ;
#12793=EDGE_LOOP ( 'NONE', ( #18409, #19601, #7971, #660 ) ) ;
#12813=VECTOR ( 'NONE', #18232, 1000.000000000000000 ) ;
#12827=ORIENTED_EDGE ( 'NONE', *, *, #924, .F. ) ;
#12835=FACE_BOUND ( 'NONE', #18385, .T. ) ;
#12841=DIRECTION ( 'NONE',  ( 1.000000000000000000, 3.254448077276381206E-32, 1.066788928082016908E-26 ) ) ;
#12869=CARTESIAN_POINT ( 'NONE',  ( 24.74999999999996447, 1.500000000000098588, -17.00000000000001066 ) ) ;
#12876=CARTESIAN_POINT ( 'NONE',  ( 0.2500000000000036637, 2.000000000000001776, -17.75000000000000711 ) ) ;
#12906=CIRCLE ( 'NONE', #11772, 1.750000000000001554 ) ;
#12935=DIRECTION ( 'NONE',  ( 1.066786462891689527E-26, 6.656013887802287108E-31, 1.000000000000000000 ) ) ;
#12940=AXIS2_PLACEMENT_3D ( 'NONE', #17575, #21119, #1359 ) ;
#12956=DIRECTION ( 'NONE',  ( -3.254448077146059901E-32, -1.000000000000000000, -6.409494854920712161E-31 ) ) ;
#12963=CYLINDRICAL_SURFACE ( 'NONE', #10206, 0.2500000000000000000 ) ;
#12965=CARTESIAN_POINT ( 'NONE',  ( 2.499999999999998668, 4.500000000000031974, -17.50000000000001776 ) ) ;
#12973=DIRECTION ( 'NONE',  ( -1.000000000000000000, 9.637352644315586861E-16, 0.000000000000000000 ) ) ;
#12977=FILL_AREA_STYLE ('',( #14504 ) ) ;
#13052=CYLINDRICAL_SURFACE ( 'NONE', #5164, 0.5000000000000000000 ) ;
#13062=AXIS2_PLACEMENT_3D ( 'NONE', #1079, #19176, #17165 ) ;
#13072=DIRECTION ( 'NONE',  ( 1.000000000000000000, 0.000000000000000000, 0.000000000000000000 ) ) ;
#13091=ORIENTED_EDGE ( 'NONE', *, *, #14411, .F. ) ;
#13096=CARTESIAN_POINT ( 'NONE',  ( 24.74999999999997158, 1.999999999999988010, -18.99999999999998224 ) ) ;
#13098=ORIENTED_EDGE ( 'NONE', *, *, #11871, .F. ) ;
#13115=DIRECTION ( 'NONE',  ( -1.000000000000000000, -3.254448077276381206E-32, -1.066788928082016908E-26 ) ) ;
#13116=ORIENTED_EDGE ( 'NONE', *, *, #14411, .T. ) ;
#13121=ADVANCED_FACE ( 'NONE', ( #18947 ), #13417, .T. ) ;
#13125=ORIENTED_EDGE ( 'NONE', *, *, #1659, .T. ) ;
#13126=ORIENTED_EDGE ( 'NONE', *, *, #14163, .F. ) ;
#13134=ADVANCED_FACE ( 'NONE', ( #4341 ), #2763, .T. ) ;
#13147=EDGE_CURVE ( 'NONE', #6184, #13207, #13535, .T. ) ;
#13155=ORIENTED_EDGE ( 'NONE', *, *, #15118, .T. ) ;
#13158=CARTESIAN_POINT ( 'NONE',  ( 22.49999999999994671, 4.500000000000059508, -18.99999999999998224 ) ) ;
#13167=CYLINDRICAL_SURFACE ( 'NONE', #8178, 4.750000000000000888 ) ;
#13199=ORIENTED_EDGE ( 'NONE', *, *, #5238, .F. ) ;
#13207=VERTEX_POINT ( 'NONE', #19173 ) ;
#13234=VERTEX_POINT ( 'NONE', #15402 ) ;
#13241=DIRECTION ( 'NONE',  ( -1.066786462891689527E-26, -6.656013887802287108E-31, -1.000000000000000000 ) ) ;
#13248=CYLINDRICAL_SURFACE ( 'NONE', #7583, 2.500000000000003553 ) ;
#13292=CIRCLE ( 'NONE', #3540, 2.000000000000000000 ) ;
#13308=AXIS2_PLACEMENT_3D ( 'NONE', #22866, #21099, #8402 ) ;
#13324=VERTEX_POINT ( 'NONE', #1647 ) ;
#13367=PLANE ( 'NONE',  #13991 ) ;
#13369=CARTESIAN_POINT ( 'NONE',  ( 2.499999999999992006, 2.000000000000001776, -3.469446951953614189E-14 ) ) ;
#13380=ORIENTED_EDGE ( 'NONE', *, *, #15969, .T. ) ;
#13408=ORIENTED_EDGE ( 'NONE', *, *, #18595, .F. ) ;
#13417=CYLINDRICAL_SURFACE ( 'NONE', #18174, 2.500000000000002220 ) ;
#13462=DIRECTION ( 'NONE',  ( 1.000000000000000000, 3.254448077276381206E-32, 1.066788928082016908E-26 ) ) ;
#13512=CARTESIAN_POINT ( 'NONE',  ( -1.387778780781445676E-14, 0.2500000000000140998, -2.000000000000001776 ) ) ;
#13535=LINE ( 'NONE', #2831, #21780 ) ;
#13554=SHAPE_REPRESENTATION_RELATIONSHIP ( 'NONE' , 'NONE' ,  #16457, #15637 ) ;
#13555=EDGE_CURVE ( 'NONE', #1275, #9105, #18035, .T. ) ;
#13563=DIRECTION ( 'NONE',  ( -1.000000000000000000, -3.254448077276381206E-32, -1.066788928082016908E-26 ) ) ;
#13587=ORIENTED_EDGE ( 'NONE', *, *, #1879, .F. ) ;
#13590=ORIENTED_EDGE ( 'NONE', *, *, #13147, .F. ) ;
#13594=CIRCLE ( 'NONE', #17715, 0.2500000000000003331 ) ;
#13621=DIRECTION ( 'NONE',  ( -1.000000000000000000, -3.254448077276381206E-32, -1.066788928082016908E-26 ) ) ;
#13656=CARTESIAN_POINT ( 'NONE',  ( 3.469446951953614189E-15, 0.2500000000000002220, -17.00000000000000711 ) ) ;
#13704=ORIENTED_EDGE ( 'NONE', *, *, #18595, .T. ) ;
#13767=AXIS2_PLACEMENT_3D ( 'NONE', #19480, #19591, #7146 ) ;
#13785=ORIENTED_EDGE ( 'NONE', *, *, #19578, .F. ) ;
#13802=DIRECTION ( 'NONE',  ( 3.254448077146059901E-32, 1.000000000000000000, 6.409494854920712161E-31 ) ) ;
#13832=AXIS2_PLACEMENT_3D ( 'NONE', #21805, #5810, #12973 ) ;
#13837=ORIENTED_EDGE ( 'NONE', *, *, #22604, .F. ) ;
#13839=CARTESIAN_POINT ( 'NONE',  ( -1.734723475976807094E-14, 2.000000000000001776, -17.00000000000000711 ) ) ;
#13890=DIRECTION ( 'NONE',  ( -1.066786462891689527E-26, -6.656013887802287108E-31, -1.000000000000000000 ) ) ;
#13915=CARTESIAN_POINT ( 'NONE',  ( 12.49999999999995914, 2.775557561562891351E-14, -9.500000000000003553 ) ) ;
#13944=EDGE_LOOP ( 'NONE', ( #18272, #4983, #4308, #3264 ) ) ;
#13951=CIRCLE ( 'NONE', #22236, 2.250000000000003109 ) ;
#13957=CARTESIAN_POINT ( 'NONE',  ( 12.49999999999996625, 0.2500000000000002220, -9.500000000000003553 ) ) ;
#13966=CARTESIAN_POINT ( 'NONE',  ( 22.50000000000003908, 4.500000000000031974, -1.249999999999997558 ) ) ;
#13973=DIRECTION ( 'NONE',  ( 1.066786462891689527E-26, 6.656013887802287108E-31, 1.000000000000000000 ) ) ;
#13991=AXIS2_PLACEMENT_3D ( 'NONE', #22543, #10068, #15465 ) ;
#13998=CARTESIAN_POINT ( 'NONE',  ( 0.2499999999999655276, 1.500000000000056843, 0.000000000000000000 ) ) ;
#14001=CARTESIAN_POINT ( 'NONE',  ( -6.591949208711866959E-14, 4.250000000000017764, -18.75000000000001066 ) ) ;
#14011=AXIS2_PLACEMENT_3D ( 'NONE', #11586, #13241, #1135 ) ;
#14017=ORIENTED_EDGE ( 'NONE', *, *, #19319, .T. ) ;
#14041=CARTESIAN_POINT ( 'NONE',  ( 12.49999999999997335, 1.500000000000015099, -9.500000000000001776 ) ) ;
#14092=VECTOR ( 'NONE', #19045, 1000.000000000000000 ) ;
#14099=CARTESIAN_POINT ( 'NONE',  ( -1.734723475976807094E-14, 2.000000000000001776, -17.00000000000000711 ) ) ;
#14107=ORIENTED_EDGE ( 'NONE', *, *, #23048, .T. ) ;
#14140=EDGE_CURVE ( 'NONE', #13234, #9677, #4005, .T. ) ;
#14144=DIRECTION ( 'NONE',  ( 1.000000000000000000, 3.254448077276381206E-32, 1.066788928082016908E-26 ) ) ;
#14159=DIRECTION ( 'NONE',  ( -3.254448077146059901E-32, -1.000000000000000000, -6.409494854920712161E-31 ) ) ;
#14163=EDGE_CURVE ( 'NONE', #4569, #4546, #12408, .T. ) ;
#14166=ORIENTED_EDGE ( 'NONE', *, *, #6144, .F. ) ;
#14168=ORIENTED_EDGE ( 'NONE', *, *, #9391, .F. ) ;
#14215=FACE_OUTER_BOUND ( 'NONE', #21467, .T. ) ;
#14230=VECTOR ( 'NONE', #1957, 1000.000000000000000 ) ;
#14240=EDGE_CURVE ( 'NONE', #20477, #13207, #17287, .T. ) ;
#14252=PRODUCT_CONTEXT ( 'NONE', #12026, 'mechanical' ) ;
#14266=ADVANCED_FACE ( 'NONE', ( #12835, #12604 ), #491, .T. ) ;
#14276=EDGE_CURVE ( 'NONE', #17281, #14364, #21056, .T. ) ;
#14279=EDGE_CURVE ( 'NONE', #22552, #9468, #20256, .T. ) ;
#14281=ORIENTED_EDGE ( 'NONE', *, *, #17570, .F. ) ;
#14289=EDGE_LOOP ( 'NONE', ( #3246, #11085, #62, #8204 ) ) ;
#14359=ORIENTED_EDGE ( 'NONE', *, *, #1659, .F. ) ;
#14364=VERTEX_POINT ( 'NONE', #15289 ) ;
#14378=CIRCLE ( 'NONE', #17373, 0.2500000000000003331 ) ;
#14411=EDGE_CURVE ( 'NONE', #21027, #20477, #4535, .T. ) ;
#14421=DIRECTION ( 'NONE',  ( 3.254448077146059901E-32, 1.000000000000000000, 6.409494854920712161E-31 ) ) ;
#14424=AXIS2_PLACEMENT_3D ( 'NONE', #18566, #2217, #16326 ) ;
#14493=CARTESIAN_POINT ( 'NONE',  ( 0.000000000000000000, 0.000000000000000000, 0.000000000000000000 ) ) ;
#14501=CARTESIAN_POINT ( 'NONE',  ( -2.081668171172168513E-14, 2.000000000000001776, -0.2500000000000002220 ) ) ;
#14504=FILL_AREA_STYLE_COLOUR ( '', #4110 ) ;
#14519=PRODUCT_DEFINITION ( 'UNKNOWN', '', #10138, #18521 ) ;
#14528=EDGE_CURVE ( 'NONE', #12123, #21498, #19291, .T. ) ;
#14535=ORIENTED_EDGE ( 'NONE', *, *, #22905, .T. ) ;
#14542=CARTESIAN_POINT ( 'NONE',  ( 24.75000000000002487, 1.250000000000001110, -2.000000000000005329 ) ) ;
#14565=ORIENTED_EDGE ( 'NONE', *, *, #20189, .F. ) ;
#14625=EDGE_LOOP ( 'NONE', ( #3798, #17304, #11661, #13408 ) ) ;
#14675=EDGE_CURVE ( 'NONE', #19219, #20477, #16211, .T. ) ;
#14694=DIRECTION ( 'NONE',  ( 0.000000000000000000, 8.673617379884027583E-16, 1.000000000000000000 ) ) ;
#14717=DIRECTION ( 'NONE',  ( 1.066786462891689527E-26, 6.656013887802287108E-31, 1.000000000000000000 ) ) ;
#14720=DIRECTION ( 'NONE',  ( 1.066786462891689527E-26, 6.656013887802287108E-31, 1.000000000000000000 ) ) ;
#14736=AXIS2_PLACEMENT_3D ( 'NONE', #13915, #19330, #17317 ) ;
#14758=UNCERTAINTY_MEASURE_WITH_UNIT (LENGTH_MEASURE( 1.000000000000000082E-05 ), #9214, 'distance_accuracy_value', 'NONE');
#14759=TOROIDAL_SURFACE ( 'NONE', #7625, 2.250000000000000444, 0.2500000000000000000 ) ;
#14781=FACE_OUTER_BOUND ( 'NONE', #16972, .T. ) ;
#14834=DIRECTION ( 'NONE',  ( 1.066786462891689527E-26, 6.656013887802287108E-31, 1.000000000000000000 ) ) ;
#14843=CARTESIAN_POINT ( 'NONE',  ( 24.99999999999995737, 2.000000000000001776, -17.49999999999998224 ) ) ;
#14855=ORIENTED_EDGE ( 'NONE', *, *, #6455, .F. ) ;
#14872=LINE ( 'NONE', #20292, #19694 ) ;
#14906=ADVANCED_FACE ( 'NONE', ( #12193 ), #1189, .T. ) ;
#14911=EDGE_LOOP ( 'NONE', ( #22963, #3054, #10716, #14281 ) ) ;
#14912=CARTESIAN_POINT ( 'NONE',  ( -1.387778780781445676E-14, 2.000000000000001776, -2.000000000000001776 ) ) ;
#14915=CARTESIAN_POINT ( 'NONE',  ( -1.387778780781445676E-14, 0.2500000000000140998, 0.000000000000000000 ) ) ;
#14926=DIRECTION ( 'NONE',  ( -1.066605682267575422E-26, 0.000000000000000000, -1.000000000000000000 ) ) ;
#14943=DIRECTION ( 'NONE',  ( 0.000000000000000000, 0.000000000000000000, 1.000000000000000000 ) ) ;
#14953=AXIS2_PLACEMENT_3D ( 'NONE', #6006, #20348, #14694 ) ;
#14965=ORIENTED_EDGE ( 'NONE', *, *, #13147, .T. ) ;
#14974=AXIS2_PLACEMENT_3D ( 'NONE', #17987, #8811, #9158 ) ;
#14980=DIRECTION ( 'NONE',  ( -1.066786462891689527E-26, -6.656013887802287108E-31, -1.000000000000000000 ) ) ;
#14991=VERTEX_POINT ( 'NONE', #21514 ) ;
#15007=DIRECTION ( 'NONE',  ( -1.000000000000000000, 0.000000000000000000, -1.066687855278535322E-26 ) ) ;
#15024=DIRECTION ( 'NONE',  ( 1.000000000000000000, 3.254448077276381206E-32, 1.066788928082016908E-26 ) ) ;
#15030=DIRECTION ( 'NONE',  ( -1.066788928082016908E-26, -3.471809175856251779E-58, 1.000000000000000000 ) ) ;
#15059=DIRECTION ( 'NONE',  ( -3.254448077146059901E-32, -1.000000000000000000, 6.656013887802287108E-31 ) ) ;
#15105=ADVANCED_FACE ( 'NONE', ( #14781 ), #13248, .T. ) ;
#15118=EDGE_CURVE ( 'NONE', #800, #4569, #13951, .T. ) ;
#15128=TOROIDAL_SURFACE ( 'NONE', #6881, 2.250000000000000444, 0.2500000000000000000 ) ;
#15129=AXIS2_PLACEMENT_3D ( 'NONE', #17071, #22391, #15315 ) ;
#15130=LINE ( 'NONE', #22323, #4441 ) ;
#15133=EDGE_CURVE ( 'NONE', #13324, #800, #2305, .T. ) ;
#15167=AXIS2_PLACEMENT_3D ( 'NONE', #14912, #5755, #19871 ) ;
#15182=CARTESIAN_POINT ( 'NONE',  ( 22.49999999999998224, 2.000000000000001776, -2.081668171172168513E-14 ) ) ;
#15243=AXIS2_PLACEMENT_3D ( 'NONE', #10109, #20936, #3048 ) ;
#15251=VERTEX_POINT ( 'NONE', #22777 ) ;
#15284=DIRECTION ( 'NONE',  ( 1.000000000000000000, 0.000000000000000000, 1.066811114794976679E-26 ) ) ;
#15289=CARTESIAN_POINT ( 'NONE',  ( -2.428612866367529932E-14, 2.000000000000043521, -18.75000000000001066 ) ) ;
#15306=CIRCLE ( 'NONE', #12693, 4.750000000000000888 ) ;
#15315=DIRECTION ( 'NONE',  ( 0.000000000000000000, -1.734723475976807094E-15, -1.000000000000000000 ) ) ;
#15323=LINE ( 'NONE', #6620, #1973 ) ;
#15330=FACE_OUTER_BOUND ( 'NONE', #14911, .T. ) ;
#15336=ORIENTED_EDGE ( 'NONE', *, *, #7261, .F. ) ;
#15375=DIRECTION ( 'NONE',  ( 0.000000000000000000, 0.000000000000000000, -1.000000000000000000 ) ) ;
#15388=ADVANCED_FACE ( 'NONE', ( #22016 ), #12963, .T. ) ;
#15391=EDGE_CURVE ( 'NONE', #1774, #15251, #13594, .T. ) ;
#15402=CARTESIAN_POINT ( 'NONE',  ( 24.74999999999997513, 0.000000000000000000, -2.000000000000022649 ) ) ;
#15415=EDGE_CURVE ( 'NONE', #882, #20683, #19225, .T. ) ;
#15417=PLANE ( 'NONE',  #9333 ) ;
#15465=DIRECTION ( 'NONE',  ( -1.000000000000000000, -3.254448077276381206E-32, -1.066788928082016908E-26 ) ) ;
#15472=CONICAL_SURFACE ( 'NONE', #4194, 4.750000000000000888, 0.7853981633974430610 ) ;
#15519=ORIENTED_EDGE ( 'NONE', *, *, #16690, .T. ) ;
#15539=ORIENTED_EDGE ( 'NONE', *, *, #12707, .T. ) ;
#15542=ORIENTED_EDGE ( 'NONE', *, *, #11348, .F. ) ;
#15573=EDGE_LOOP ( 'NONE', ( #19976, #7131, #9277, #9365 ) ) ;
#15593=PLANE ( 'NONE',  #6156 ) ;
#15599=AXIS2_PLACEMENT_3D ( 'NONE', #20357, #11636, #8121 ) ;
#15634=CIRCLE ( 'NONE', #20914, 0.5000000000000000000 ) ;
#15637=ADVANCED_BREP_SHAPE_REPRESENTATION ( '', ( #5189, #22115 ), #4465 ) ;
#15650=ORIENTED_EDGE ( 'NONE', *, *, #811, .F. ) ;
#15651=ADVANCED_FACE ( 'NONE', ( #10908 ), #5333, .T. ) ;
#15684=ORIENTED_EDGE ( 'NONE', *, *, #22469, .T. ) ;
#15687=EDGE_CURVE ( 'NONE', #7125, #5612, #11266, .T. ) ;
#15694=CARTESIAN_POINT ( 'NONE',  ( 24.75000000000000355, 2.000000000000029310, -0.2500000000000002220 ) ) ;
#15705=ADVANCED_FACE ( 'NONE', ( #2088 ), #22214, .T. ) ;
#15744=DIRECTION ( 'NONE',  ( 1.000000000000000000, 3.254448077276381206E-32, 1.066788928082016908E-26 ) ) ;
#15753=MECHANICAL_DESIGN_GEOMETRIC_PRESENTATION_REPRESENTATION('',(#9018),#7153);
#15761=FACE_OUTER_BOUND ( 'NONE', #13944, .T. ) ;
#15784=LINE ( 'NONE', #11802, #4586 ) ;
#15803=CARTESIAN_POINT ( 'NONE',  ( 25.00000000000000355, 2.000000000000001776, 0.000000000000000000 ) ) ;
#15828=CARTESIAN_POINT ( 'NONE',  ( 0.2499999999999898137, 1.500000000000029088, -17.00000000000000711 ) ) ;
#15837=DIRECTION ( 'NONE',  ( 1.000000000000000000, -7.100545512326564696E-57, -1.066786462891689527E-26 ) ) ;
#15849=ORIENTED_EDGE ( 'NONE', *, *, #52, .F. ) ;
#15871=CIRCLE ( 'NONE', #18901, 0.2500000000000002220 ) ;
#15903=DIRECTION ( 'NONE',  ( 3.254448077146059901E-32, 1.000000000000000000, 6.409494854920712161E-31 ) ) ;
#15917=ORIENTED_EDGE ( 'NONE', *, *, #8666, .F. ) ;
#15923=TOROIDAL_SURFACE ( 'NONE', #5813, 1.750000000000000000, 0.2500000000000000000 ) ;
#15969=EDGE_CURVE ( 'NONE', #1774, #2242, #2328, .T. ) ;
#16004=VERTEX_POINT ( 'NONE', #10554 ) ;
#16064=DIRECTION ( 'NONE',  ( 0.000000000000000000, 0.000000000000000000, -1.000000000000000000 ) ) ;
#16081=CARTESIAN_POINT ( 'NONE',  ( 24.74999999999996447, 1.500000000000043077, -2.081668171172168513E-14 ) ) ;
#16088=VERTEX_POINT ( 'NONE', #8328 ) ;
#16113=ORIENTED_EDGE ( 'NONE', *, *, #5841, .T. ) ;
#16140=EDGE_CURVE ( 'NONE', #22552, #20884, #7237, .T. ) ;
#16145=ORIENTED_EDGE ( 'NONE', *, *, #3766, .T. ) ;
#16160=( NAMED_UNIT ( * ) SI_UNIT ( $, .STERADIAN. ) SOLID_ANGLE_UNIT ( ) );
#16209=VECTOR ( 'NONE', #5638, 1000.000000000000000 ) ;
#16211=LINE ( 'NONE', #3864, #12813 ) ;
#16217=VECTOR ( 'NONE', #7817, 1000.000000000000000 ) ;
#16281=CIRCLE ( 'NONE', #9898, 0.2500000000000002220 ) ;
#16283=AXIS2_PLACEMENT_3D ( 'NONE', #8218, #8329, #3039 ) ;
#16326=DIRECTION ( 'NONE',  ( -1.000000000000000000, 0.000000000000000000, 0.000000000000000000 ) ) ;
#16344=CARTESIAN_POINT ( 'NONE',  ( -1.387778780781445676E-14, 2.000000000000001776, -1.500000000000001332 ) ) ;
#16407=TOROIDAL_SURFACE ( 'NONE', #11541, 0.7500000000000000000, 0.2500000000000000000 ) ;
#16416=CIRCLE ( 'NONE', #19812, 2.500000000000002220 ) ;
#16438=LINE ( 'NONE', #21985, #18643 ) ;
#16457=SHAPE_REPRESENTATION ( 'Bracket washer', ( #22115 ), #4465 ) ;
#16464=EDGE_CURVE ( 'NONE', #21027, #20045, #22542, .T. ) ;
#16472=CARTESIAN_POINT ( 'NONE',  ( 0.2499999999999932832, 2.775557561562891351E-14, -2.000000000000001776 ) ) ;
#16485=ORIENTED_EDGE ( 'NONE', *, *, #16914, .T. ) ;
#16501=DIRECTION ( 'NONE',  ( 1.000000000000000000, 3.254448077276381206E-32, 1.066788928082016908E-26 ) ) ;
#16513=VERTEX_POINT ( 'NONE', #18063 ) ;
#16535=EDGE_CURVE ( 'NONE', #21498, #9105, #19942, .T. ) ;
#16565=ADVANCED_FACE ( 'NONE', ( #17941 ), #4592, .T. ) ;
#16584=CARTESIAN_POINT ( 'NONE',  ( 0.2500000000000071609, 2.000000000000001776, 0.000000000000000000 ) ) ;
#16603=ORIENTED_EDGE ( 'NONE', *, *, #7395, .T. ) ;
#16604=ORIENTED_EDGE ( 'NONE', *, *, #8640, .F. ) ;
#16623=UNCERTAINTY_MEASURE_WITH_UNIT (LENGTH_MEASURE( 1.000000000000000082E-05 ), #16715, 'distance_accuracy_value', 'NONE');
#16642=DIRECTION ( 'NONE',  ( -1.066786462891689527E-26, -6.656013887802287108E-31, -1.000000000000000000 ) ) ;
#16647=CIRCLE ( 'NONE', #910, 4.750000000000000888 ) ;
#16672=DIRECTION ( 'NONE',  ( 3.254448077146059901E-32, 1.000000000000000000, 6.409494854920712161E-31 ) ) ;
#16690=EDGE_CURVE ( 'NONE', #4569, #11578, #531, .T. ) ;
#16702=DIRECTION ( 'NONE',  ( -1.066194817212773768E-26, 0.000000000000000000, -1.000000000000000000 ) ) ;
#16715=( LENGTH_UNIT ( ) NAMED_UNIT ( * ) SI_UNIT ( .MILLI., .METRE. ) );
#16736=CIRCLE ( 'NONE', #18355, 0.2500000000000002220 ) ;
#16745=EDGE_LOOP ( 'NONE', ( #5060, #6417, #4391, #22303 ) ) ;
#16793=CIRCLE ( 'NONE', #7058, 2.500000000000002220 ) ;
#16810=EDGE_CURVE ( 'NONE', #10973, #19482, #15323, .T. ) ;
#16854=EDGE_CURVE ( 'NONE', #7230, #7125, #12508, .T. ) ;
#16864=AXIS2_PLACEMENT_3D ( 'NONE', #8974, #19792, #10607 ) ;
#16869=ORIENTED_EDGE ( 'NONE', *, *, #21629, .T. ) ;
#16900=DIRECTION ( 'NONE',  ( -1.000000000000000000, 0.000000000000000000, 0.000000000000000000 ) ) ;
#16913=CARTESIAN_POINT ( 'NONE',  ( 12.49999999999995914, 1.250000000000015099, -4.750000000000000888 ) ) ;
#16914=EDGE_CURVE ( 'NONE', #20423, #13234, #15871, .T. ) ;
#16924=DIRECTION ( 'NONE',  ( -1.066786462891689527E-26, -6.656013887802287108E-31, -1.000000000000000000 ) ) ;
#16966=CARTESIAN_POINT ( 'NONE',  ( 2.499999999999988454, 4.500000000000059508, -1.250000000000028866 ) ) ;
#16972=EDGE_LOOP ( 'NONE', ( #21316, #6212, #826, #2553 ) ) ;
#16973=ORIENTED_EDGE ( 'NONE', *, *, #5353, .T. ) ;
#17013=ORIENTED_EDGE ( 'NONE', *, *, #9386, .F. ) ;
#17044=EDGE_CURVE ( 'NONE', #14991, #3633, #11749, .T. ) ;
#17053=DIRECTION ( 'NONE',  ( 1.000000000000000000, -7.100545512326564696E-57, -1.066786462891689527E-26 ) ) ;
#17058=CARTESIAN_POINT ( 'NONE',  ( -2.081668171172168513E-14, 2.000000000000001776, -1.250000000000001110 ) ) ;
#17071=CARTESIAN_POINT ( 'NONE',  ( 0.2500000000000071609, 2.000000000000001776, -1.250000000000001110 ) ) ;
#17073=ORIENTED_EDGE ( 'NONE', *, *, #9477, .T. ) ;
#17080=CARTESIAN_POINT ( 'NONE',  ( 24.75000000000001066, 2.000000000000099032, -17.74999999999998224 ) ) ;
#17150=CARTESIAN_POINT ( 'NONE',  ( 22.49999999999993960, 4.250000000000045297, -17.50000000000001066 ) ) ;
#17155=ORIENTED_EDGE ( 'NONE', *, *, #16464, .T. ) ;
#17158=ORIENTED_EDGE ( 'NONE', *, *, #15687, .T. ) ;
#17165=DIRECTION ( 'NONE',  ( -1.000000000000000000, 0.000000000000000000, 0.000000000000000000 ) ) ;
#17229=DIRECTION ( 'NONE',  ( 1.066786462891689527E-26, 6.656013887802287108E-31, 1.000000000000000000 ) ) ;
#17252=CARTESIAN_POINT ( 'NONE',  ( 2.499999999999992006, 2.000000000000001776, -1.250000000000028866 ) ) ;
#17266=CARTESIAN_POINT ( 'NONE',  ( 12.49999999999995914, 2.775557561562891036E-14, -14.50000000000000355 ) ) ;
#17281=VERTEX_POINT ( 'NONE', #1653 ) ;
#17287=CIRCLE ( 'NONE', #5660, 0.2500000000000000000 ) ;
#17304=ORIENTED_EDGE ( 'NONE', *, *, #17939, .F. ) ;
#17317=DIRECTION ( 'NONE',  ( 0.000000000000000000, -6.162975822039153854E-31, -1.000000000000000000 ) ) ;
#17332=AXIS2_PLACEMENT_3D ( 'NONE', #9700, #20526, #11330 ) ;
#17349=CIRCLE ( 'NONE', #9858, 1.750000000000000000 ) ;
#17373=AXIS2_PLACEMENT_3D ( 'NONE', #18650, #7949, #22305 ) ;
#17374=VECTOR ( 'NONE', #4380, 1000.000000000000000 ) ;
#17376=DIRECTION ( 'NONE',  ( 3.254448077146059901E-32, 1.000000000000000000, 6.409494854920712161E-31 ) ) ;
#17383=ORIENTED_EDGE ( 'NONE', *, *, #17044, .F. ) ;
#17422=EDGE_LOOP ( 'NONE', ( #3805, #6726, #20247, #1576 ) ) ;
#17437=CARTESIAN_POINT ( 'NONE',  ( 25.00000000000001776, 1.250000000000028866, -2.000000000000005329 ) ) ;
#17445=DIRECTION ( 'NONE',  ( 3.254448077146059901E-32, 1.000000000000000000, 6.409494854920712161E-31 ) ) ;
#17491=( GEOMETRIC_REPRESENTATION_CONTEXT ( 3 ) GLOBAL_UNCERTAINTY_ASSIGNED_CONTEXT ( ( #7685 ) ) GLOBAL_UNIT_ASSIGNED_CONTEXT ( ( #3474, #10759, #16160 ) ) REPRESENTATION_CONTEXT ( 'NONE', 'WORKASPACE' ) );
#17502=VECTOR ( 'NONE', #21050, 999.9999999999998863 ) ;
#17503=DIRECTION ( 'NONE',  ( -1.066786462891689527E-26, -6.656013887802287108E-31, -1.000000000000000000 ) ) ;
#17510=VECTOR ( 'NONE', #21295, 1000.000000000000000 ) ;
#17525=CARTESIAN_POINT ( 'NONE',  ( 22.49999999999998224, 2.000000000000001776, -0.2500000000000210387 ) ) ;
#17535=ORIENTED_EDGE ( 'NONE', *, *, #19668, .T. ) ;
#17570=EDGE_CURVE ( 'NONE', #21116, #16513, #5120, .T. ) ;
#17575=CARTESIAN_POINT ( 'NONE',  ( 24.75000000000002487, 1.250000000000001110, -2.081668171172168513E-14 ) ) ;
#17596=CIRCLE ( 'NONE', #21383, 2.250000000000001776 ) ;
#17599=CIRCLE ( 'NONE', #5196, 0.2500000000000000000 ) ;
#17624=DIRECTION ( 'NONE',  ( 1.066788928082016908E-26, -6.656013887802287108E-31, -1.000000000000000000 ) ) ;
#17639=CARTESIAN_POINT ( 'NONE',  ( 25.00000000000000355, 2.000000000000001776, -2.000000000000005329 ) ) ;
#17641=DIRECTION ( 'NONE',  ( 1.066786462891689527E-26, 6.656013887802287108E-31, 1.000000000000000000 ) ) ;
#17685=EDGE_CURVE ( 'NONE', #7941, #20683, #16281, .T. ) ;
#17699=CARTESIAN_POINT ( 'NONE',  ( 12.49999999999992362, 1.250000000000015099, -4.750000000000000888 ) ) ;
#17700=CARTESIAN_POINT ( 'NONE',  ( 0.2499999999999828748, 0.2500000000000418554, -17.00000000000000711 ) ) ;
#17711=ORIENTED_EDGE ( 'NONE', *, *, #10792, .F. ) ;
#17715=AXIS2_PLACEMENT_3D ( 'NONE', #17700, #20138, #5250 ) ;
#17744=EDGE_CURVE ( 'NONE', #7941, #14364, #14872, .T. ) ;
#17746=TOROIDAL_SURFACE ( 'NONE', #12082, 0.7500000000000000000, 0.2500000000000000000 ) ;
#17755=CIRCLE ( 'NONE', #5757, 0.2500000000000000000 ) ;
#17773=AXIS2_PLACEMENT_3D ( 'NONE', #493, #2124, #4346 ) ;
#17795=CARTESIAN_POINT ( 'NONE',  ( 22.49999999999998934, 4.250000000000017764, -19.00000000000001421 ) ) ;
#17822=VERTEX_POINT ( 'NONE', #5940 ) ;
#17905=ORIENTED_EDGE ( 'NONE', *, *, #5357, .F. ) ;
#17920=CIRCLE ( 'NONE', #13767, 5.000000000000000888 ) ;
#17928=EDGE_LOOP ( 'NONE', ( #21327, #13587, #10744, #19083 ) ) ;
#17939=EDGE_CURVE ( 'NONE', #20683, #12123, #11411, .T. ) ;
#17941=FACE_OUTER_BOUND ( 'NONE', #15573, .T. ) ;
#17944=CARTESIAN_POINT ( 'NONE',  ( 22.49999999999992539, 1.999999999999960032, -18.75000000000001421 ) ) ;
#17946=SURFACE_STYLE_FILL_AREA ( #19824 ) ;
#17959=DIRECTION ( 'NONE',  ( 3.254448077146059901E-32, 1.000000000000000000, -6.656013887802287108E-31 ) ) ;
#17975=AXIS2_PLACEMENT_3D ( 'NONE', #7042, #19848, #9144 ) ;
#17987=CARTESIAN_POINT ( 'NONE',  ( 2.499999999999984901, 2.000000000000001776, -1.500000000000029088 ) ) ;
#18035=CIRCLE ( 'NONE', #26, 0.5000000000000000000 ) ;
#18048=ORIENTED_EDGE ( 'NONE', *, *, #8096, .T. ) ;
#18063=CARTESIAN_POINT ( 'NONE',  ( 12.49999999999992362, 1.500000000000015099, -4.500000000000003553 ) ) ;
#18094=PLANE ( 'NONE',  #9342 ) ;
#18098=EDGE_LOOP ( 'NONE', ( #15849, #7857, #8789, #12538 ) ) ;
#18100=DIRECTION ( 'NONE',  ( -1.000000000000000000, 0.000000000000000000, -1.066788928082016908E-26 ) ) ;
#18101=EDGE_LOOP ( 'NONE', ( #18797, #9393, #9499, #7001 ) ) ;
#18113=CARTESIAN_POINT ( 'NONE',  ( -2.081668171172168513E-14, 1.250000000000001110, -2.000000000000001776 ) ) ;
#18125=AXIS2_PLACEMENT_3D ( 'NONE', #4790, #20691, #16900 ) ;
#18141=DIRECTION ( 'NONE',  ( 0.000000000000000000, 0.000000000000000000, 1.000000000000000000 ) ) ;
#18148=DIRECTION ( 'NONE',  ( 1.066788928082016908E-26, 3.471809175856251779E-58, -1.000000000000000000 ) ) ;
#18160=CIRCLE ( 'NONE', #20042, 0.2500000000000002220 ) ;
#18161=EDGE_LOOP ( 'NONE', ( #16145, #4891, #22144, #16603 ) ) ;
#18174=AXIS2_PLACEMENT_3D ( 'NONE', #8007, #22241, #15284 ) ;
#18200=ORIENTED_EDGE ( 'NONE', *, *, #19668, .F. ) ;
#18225=DIRECTION ( 'NONE',  ( 1.000000000000000000, 3.254448077276381206E-32, 1.066788928082016908E-26 ) ) ;
#18232=DIRECTION ( 'NONE',  ( -1.066786462891689527E-26, -6.656013887802287108E-31, -1.000000000000000000 ) ) ;
#18242=ORIENTED_EDGE ( 'NONE', *, *, #11532, .T. ) ;
#18245=ORIENTED_EDGE ( 'NONE', *, *, #7013, .T. ) ;
#18269=ADVANCED_FACE ( 'NONE', ( #7555 ), #20139, .T. ) ;
#18272=ORIENTED_EDGE ( 'NONE', *, *, #5238, .T. ) ;
#18301=CIRCLE ( 'NONE', #661, 0.7499999999999997780 ) ;
#18315=AXIS2_PLACEMENT_3D ( 'NONE', #874, #11675, #11799 ) ;
#18319=CARTESIAN_POINT ( 'NONE',  ( 1.040834085586084257E-14, 1.500000000000029088, -17.00000000000000711 ) ) ;
#18355=AXIS2_PLACEMENT_3D ( 'NONE', #6249, #18827, #14943 ) ;
#18385=EDGE_LOOP ( 'NONE', ( #7653, #16869 ) ) ;
#18396=DIRECTION ( 'NONE',  ( 8.659560563109223167E-17, -0.7071067811865516806, 0.7071067811865434649 ) ) ;
#18405=LINE ( 'NONE', #9811, #16217 ) ;
#18409=ORIENTED_EDGE ( 'NONE', *, *, #20155, .F. ) ;
#18411=CARTESIAN_POINT ( 'NONE',  ( -1.734723475976807094E-14, 2.000000000000001776, -17.75000000000000711 ) ) ;
#18449=CARTESIAN_POINT ( 'NONE',  ( 24.75000000000000355, 2.000000000000029310, -2.000000000000005329 ) ) ;
#18451=ADVANCED_FACE ( 'NONE', ( #15761 ), #5391, .T. ) ;
#18456=CARTESIAN_POINT ( 'NONE',  ( -1.387778780781445676E-14, 2.000000000000001776, -1.500000000000001332 ) ) ;
#18467=CIRCLE ( 'NONE', #17332, 0.2500000000000002220 ) ;
#18469=ORIENTED_EDGE ( 'NONE', *, *, #22498, .T. ) ;
#18475=ORIENTED_EDGE ( 'NONE', *, *, #16464, .F. ) ;
#18483=DIRECTION ( 'NONE',  ( 1.066811114794977684E-26, 0.000000000000000000, 1.000000000000000000 ) ) ;
#18485=CYLINDRICAL_SURFACE ( 'NONE', #8919, 2.500000000000002220 ) ;
#18521=PRODUCT_DEFINITION_CONTEXT ( 'detailed design', #8638, 'design' ) ;
#18529=VECTOR ( 'NONE', #22616, 1000.000000000000000 ) ;
#18537=ORIENTED_EDGE ( 'NONE', *, *, #21775, .T. ) ;
#18566=CARTESIAN_POINT ( 'NONE',  ( 0.2499999999999932832, 1.250000000000042633, -2.000000000000001776 ) ) ;
#18567=CARTESIAN_POINT ( 'NONE',  ( 2.499999999999981348, 4.250000000000087041, -17.50000000000001776 ) ) ;
#18569=ORIENTED_EDGE ( 'NONE', *, *, #11871, .T. ) ;
#18580=FACE_OUTER_BOUND ( 'NONE', #8268, .T. ) ;
#18595=EDGE_CURVE ( 'NONE', #23027, #7941, #1308, .T. ) ;
#18643=VECTOR ( 'NONE', #18225, 1000.000000000000000 ) ;
#18650=CARTESIAN_POINT ( 'NONE',  ( 0.2499999999999516498, 0.2500000000000140998, -2.000000000000001776 ) ) ;
#18677=CIRCLE ( 'NONE', #659, 0.2500000000000000000 ) ;
#18685=CIRCLE ( 'NONE', #682, 2.000000000000000000 ) ;
#18740=AXIS2_PLACEMENT_3D ( 'NONE', #5514, #12676, #5039 ) ;
#18784=EDGE_CURVE ( 'NONE', #4468, #8523, #18160, .T. ) ;
#18797=ORIENTED_EDGE ( 'NONE', *, *, #7960, .T. ) ;
#18802=CYLINDRICAL_SURFACE ( 'NONE', #12091, 2.500000000000003553 ) ;
#18803=CARTESIAN_POINT ( 'NONE',  ( 12.49999999999995914, 2.775557561562891036E-14, -4.500000000000002665 ) ) ;
#18827=DIRECTION ( 'NONE',  ( -1.000000000000000000, -3.254448077276381206E-32, -1.066788928082016908E-26 ) ) ;
#18830=CARTESIAN_POINT ( 'NONE',  ( 12.49999999999995914, 2.775557561562891351E-14, -9.500000000000003553 ) ) ;
#18847=LINE ( 'NONE', #4496, #18529 ) ;
#18854=CARTESIAN_POINT ( 'NONE',  ( 22.49999999999993960, 4.250000000000045297, -17.75000000000001066 ) ) ;
#18874=ORIENTED_EDGE ( 'NONE', *, *, #8096, .F. ) ;
#18901=AXIS2_PLACEMENT_3D ( 'NONE', #19790, #3442, #21225 ) ;
#18905=AXIS2_PLACEMENT_3D ( 'NONE', #17080, #4739, #11907 ) ;
#18910=CARTESIAN_POINT ( 'NONE',  ( 2.499999999999988454, 4.500000000000059508, -1.250000000000028866 ) ) ;
#18918=ORIENTED_EDGE ( 'NONE', *, *, #16914, .F. ) ;
#18947=FACE_OUTER_BOUND ( 'NONE', #19274, .T. ) ;
#19045=DIRECTION ( 'NONE',  ( -1.000000000000000000, -3.254448077276381206E-32, -1.066788928082016908E-26 ) ) ;
#19083=ORIENTED_EDGE ( 'NONE', *, *, #15415, .F. ) ;
#19109=TOROIDAL_SURFACE ( 'NONE', #20617, 2.250000000000000444, 0.2500000000000000000 ) ;
#19111=ORIENTED_EDGE ( 'NONE', *, *, #11532, .F. ) ;
#19118=FACE_OUTER_BOUND ( 'NONE', #2503, .T. ) ;
#19121=FACE_OUTER_BOUND ( 'NONE', #22916, .T. ) ;
#19145=DIRECTION ( 'NONE',  ( 1.000000000000000000, 0.000000000000000000, 0.000000000000000000 ) ) ;
#19167=ADVANCED_FACE ( 'NONE', ( #917 ), #15593, .T. ) ;
#19173=CARTESIAN_POINT ( 'NONE',  ( 22.49999999999999645, 4.250000000000031974, -1.499999999999997780 ) ) ;
#19176=DIRECTION ( 'NONE',  ( -1.066786462891689527E-26, -6.656013887802287108E-31, -1.000000000000000000 ) ) ;
#19185=DIRECTION ( 'NONE',  ( -1.066605682267576713E-26, 0.000000000000000000, -1.000000000000000000 ) ) ;
#19204=DIRECTION ( 'NONE',  ( 1.066786462891689527E-26, 6.656013887802287108E-31, 1.000000000000000000 ) ) ;
#19211=FACE_OUTER_BOUND ( 'NONE', #2440, .T. ) ;
#19219=VERTEX_POINT ( 'NONE', #22550 ) ;
#19225=CIRCLE ( 'NONE', #1941, 2.250000000000003109 ) ;
#19274=EDGE_LOOP ( 'NONE', ( #4136, #18469, #18475, #13116 ) ) ;
#19291=LINE ( 'NONE', #13998, #5300 ) ;
#19319=EDGE_CURVE ( 'NONE', #4569, #9677, #13292, .T. ) ;
#19330=DIRECTION ( 'NONE',  ( 3.254448077146059901E-32, 1.000000000000000000, 6.409494854920712161E-31 ) ) ;
#19332=VECTOR ( 'NONE', #9521, 1000.000000000000000 ) ;
#19335=CARTESIAN_POINT ( 'NONE',  ( 24.75000000000001066, 2.000000000000099032, -16.99999999999999289 ) ) ;
#19357=DIRECTION ( 'NONE',  ( -1.066786462891689527E-26, -6.656013887802287108E-31, -1.000000000000000000 ) ) ;
#19358=CARTESIAN_POINT ( 'NONE',  ( 0.2500000000000036637, 2.000000000000001776, -17.50000000000000711 ) ) ;
#19366=ORIENTED_EDGE ( 'NONE', *, *, #9498, .F. ) ;
#19435=DIRECTION ( 'NONE',  ( -1.000000000000000000, -3.254448077276381206E-32, -1.066788928082016908E-26 ) ) ;
#19451=EDGE_LOOP ( 'NONE', ( #1855, #18874, #13837, #14565 ) ) ;
#19470=DIRECTION ( 'NONE',  ( 1.000000000000000000, -7.100545512326564696E-57, -1.066786462891689527E-26 ) ) ;
#19478=ADVANCED_FACE ( 'NONE', ( #22625 ), #15923, .T. ) ;
#19480=CARTESIAN_POINT ( 'NONE',  ( 12.49999999999995914, 2.775557561562891351E-14, -9.500000000000003553 ) ) ;
#19482=VERTEX_POINT ( 'NONE', #17437 ) ;
#19504=FACE_OUTER_BOUND ( 'NONE', #11897, .T. ) ;
#19518=ORIENTED_EDGE ( 'NONE', *, *, #3266, .F. ) ;
#19575=EDGE_LOOP ( 'NONE', ( #12827, #22155, #3883, #58 ) ) ;
#19578=EDGE_CURVE ( 'NONE', #9677, #15251, #4737, .T. ) ;
#19582=DIRECTION ( 'NONE',  ( 1.066788928082016908E-26, 3.471809175856251779E-58, -1.000000000000000000 ) ) ;
#19591=DIRECTION ( 'NONE',  ( 3.254448077146059901E-32, 1.000000000000000000, 6.409494854920712161E-31 ) ) ;
#19601=ORIENTED_EDGE ( 'NONE', *, *, #10968, .T. ) ;
#19617=CARTESIAN_POINT ( 'NONE',  ( 25.00000000000004619, 0.2499999999999863443, -1.999999999999998224 ) ) ;
#19660=SHAPE_DEFINITION_REPRESENTATION ( #1233, #16457 ) ;
#19665=ORIENTED_EDGE ( 'NONE', *, *, #21785, .F. ) ;
#19668=EDGE_CURVE ( 'NONE', #17822, #10973, #4288, .T. ) ;
#19694=VECTOR ( 'NONE', #9699, 1000.000000000000000 ) ;
#19715=DIRECTION ( 'NONE',  ( 3.791174248318675826E-31, 1.000000000000000000, 1.734723475976803347E-15 ) ) ;
#19731=EDGE_LOOP ( 'NONE', ( #1939, #22501, #1608, #22039 ) ) ;
#19790=CARTESIAN_POINT ( 'NONE',  ( 24.75000000000001776, 0.2500000000000418554, -2.000000000000022649 ) ) ;
#19792=DIRECTION ( 'NONE',  ( -1.066786462891689527E-26, -6.656013887802287108E-31, -1.000000000000000000 ) ) ;
#19812=AXIS2_PLACEMENT_3D ( 'NONE', #2206, #6209, #21024 ) ;
#19824=FILL_AREA_STYLE ('',( #10643 ) ) ;
#19825=VECTOR ( 'NONE', #13462, 1000.000000000000000 ) ;
#19848=DIRECTION ( 'NONE',  ( -3.254448077146059901E-32, -1.000000000000000000, -6.409494854920712161E-31 ) ) ;
#19855=AXIS2_PLACEMENT_3D ( 'NONE', #17525, #13890, #21074 ) ;
#19858=CARTESIAN_POINT ( 'NONE',  ( 12.49999999999995914, 2.775557561562891982E-14, -14.50000000000000355 ) ) ;
#19865=CIRCLE ( 'NONE', #1825, 5.000000000000000888 ) ;
#19871=DIRECTION ( 'NONE',  ( -1.066723072283234472E-26, 0.000000000000000000, -1.000000000000000000 ) ) ;
#19942=LINE ( 'NONE', #187, #1600 ) ;
#19976=ORIENTED_EDGE ( 'NONE', *, *, #9386, .T. ) ;
#19986=DIRECTION ( 'NONE',  ( -1.000000000000000000, -3.254448077276381206E-32, -1.066788928082016908E-26 ) ) ;
#20027=CIRCLE ( 'NONE', #18905, 0.2500000000000002220 ) ;
#20039=ADVANCED_FACE ( 'NONE', ( #12461 ), #21308, .T. ) ;
#20042=AXIS2_PLACEMENT_3D ( 'NONE', #20829, #945, #21047 ) ;
#20045=VERTEX_POINT ( 'NONE', #1654 ) ;
#20053=CARTESIAN_POINT ( 'NONE',  ( 0.2499999999999655276, 2.000000000000015543, -1.500000000000001332 ) ) ;
#20095=CIRCLE ( 'NONE', #5076, 0.2500000000000000000 ) ;
#20129=ORIENTED_EDGE ( 'NONE', *, *, #6144, .T. ) ;
#20132=DIRECTION ( 'NONE',  ( -1.000000000000000000, -3.254448077276381206E-32, -1.066788928082016908E-26 ) ) ;
#20138=DIRECTION ( 'NONE',  ( 1.066786462891689527E-26, 6.656013887802287108E-31, 1.000000000000000000 ) ) ;
#20139=CYLINDRICAL_SURFACE ( 'NONE', #3909, 2.000000000000000000 ) ;
#20155=EDGE_CURVE ( 'NONE', #4546, #20884, #7639, .T. ) ;
#20161=VERTEX_POINT ( 'NONE', #18113 ) ;
#20189=EDGE_CURVE ( 'NONE', #7230, #882, #6456, .T. ) ;
#20232=TOROIDAL_SURFACE ( 'NONE', #19855, 2.250000000000000444, 0.2500000000000000000 ) ;
#20238=DIRECTION ( 'NONE',  ( -1.066811114794977684E-26, 0.000000000000000000, -1.000000000000000000 ) ) ;
#20247=ORIENTED_EDGE ( 'NONE', *, *, #22469, .F. ) ;
#20256=LINE ( 'NONE', #4119, #6773 ) ;
#20265=FACE_OUTER_BOUND ( 'NONE', #18161, .T. ) ;
#20272=ADVANCED_FACE ( 'NONE', ( #9757 ), #12196, .F. ) ;
#20273=SURFACE_STYLE_USAGE ( .BOTH. , #5914 ) ;
#20292=CARTESIAN_POINT ( 'NONE',  ( -2.428612866367529932E-14, 2.000000000000043521, -19.00000000000001066 ) ) ;
#20295=LINE ( 'NONE', #4159, #8142 ) ;
#20344=AXIS2_PLACEMENT_3D ( 'NONE', #20369, #15059, #4238 ) ;
#20348=DIRECTION ( 'NONE',  ( 1.000000000000000000, 3.254448077276381206E-32, 1.066788928082016908E-26 ) ) ;
#20351=ORIENTED_EDGE ( 'NONE', *, *, #6503, .T. ) ;
#20357=CARTESIAN_POINT ( 'NONE',  ( 24.99999999999998934, 1.500000000000001332, 0.000000000000000000 ) ) ;
#20369=CARTESIAN_POINT ( 'NONE',  ( -6.938893903907228378E-15, 1.500000000000001332, 0.000000000000000000 ) ) ;
#20378=CIRCLE ( 'NONE', #6470, 0.2500000000000002220 ) ;
#20393=COLOUR_RGB ( '', 0.31764706, 0.68627451, 0.89019608) ;
#20423=VERTEX_POINT ( 'NONE', #19617 ) ;
#20434=CIRCLE ( 'NONE', #16283, 2.500000000000002220 ) ;
#20444=CARTESIAN_POINT ( 'NONE',  ( 2.499999999999992006, 4.250000000000003553, -0.2500000000000349165 ) ) ;
#20457=CARTESIAN_POINT ( 'NONE',  ( 2.499999999999992006, 2.000000000000001776, -3.469446951953614189E-14 ) ) ;
#20477=VERTEX_POINT ( 'NONE', #13966 ) ;
#20517=ORIENTED_EDGE ( 'NONE', *, *, #4187, .F. ) ;
#20526=DIRECTION ( 'NONE',  ( 1.720845688168991849E-15, -1.000000000000000000, -6.656013887802284481E-31 ) ) ;
#20534=ORIENTED_EDGE ( 'NONE', *, *, #11070, .F. ) ;
#20541=AXIS2_PLACEMENT_3D ( 'NONE', #2785, #9842, #1029 ) ;
#20557=DIRECTION ( 'NONE',  ( -1.000000000000000000, -3.254448077276381206E-32, -1.066788928082016908E-26 ) ) ;
#20558=CONICAL_SURFACE ( 'NONE', #10406, 5.000000000000000888, 0.7853981633974430610 ) ;
#20617=AXIS2_PLACEMENT_3D ( 'NONE', #17944, #5477, #19470 ) ;
#20621=( NAMED_UNIT ( * ) SI_UNIT ( $, .STERADIAN. ) SOLID_ANGLE_UNIT ( ) );
#20683=VERTEX_POINT ( 'NONE', #19358 ) ;
#20690=VECTOR ( 'NONE', #3670, 1000.000000000000000 ) ;
#20691=DIRECTION ( 'NONE',  ( -1.066786462891689527E-26, -6.656013887802287108E-31, -1.000000000000000000 ) ) ;
#20697=DIRECTION ( 'NONE',  ( 7.543342432310246422E-27, 0.7071067811865516806, 0.7071067811865434649 ) ) ;
#20699=CARTESIAN_POINT ( 'NONE',  ( 12.49999999999992362, 1.250000000000015099, -9.500000000000001776 ) ) ;
#20710=ORIENTED_EDGE ( 'NONE', *, *, #17744, .T. ) ;
#20714=DIRECTION ( 'NONE',  ( 1.000000000000000000, 3.254448077276381206E-32, 1.066788928082016908E-26 ) ) ;
#20793=DIRECTION ( 'NONE',  ( -1.000000000000000000, 7.100545512326564696E-57, 1.066786462891689527E-26 ) ) ;
#20804=DIRECTION ( 'NONE',  ( -1.000000000000000000, -3.254448077276381206E-32, -1.066788928082016908E-26 ) ) ;
#20807=ORIENTED_EDGE ( 'NONE', *, *, #7649, .F. ) ;
#20826=ADVANCED_FACE ( 'NONE', ( #616, #20265 ), #7899, .F. ) ;
#20829=CARTESIAN_POINT ( 'NONE',  ( 24.74999999999997158, 1.999999999999988010, -18.74999999999998224 ) ) ;
#20832=EDGE_CURVE ( 'NONE', #4468, #17822, #503, .T. ) ;
#20856=DIRECTION ( 'NONE',  ( 1.000000000000000000, 3.254448077276381206E-32, 1.066788928082016908E-26 ) ) ;
#20861=ADVANCED_FACE ( 'NONE', ( #846 ), #18485, .T. ) ;
#20866=DIRECTION ( 'NONE',  ( 0.000000000000000000, 0.000000000000000000, 1.000000000000000000 ) ) ;
#20884=VERTEX_POINT ( 'NONE', #17058 ) ;
#20911=CYLINDRICAL_SURFACE ( 'NONE', #1460, 2.000000000000001776 ) ;
#20914=AXIS2_PLACEMENT_3D ( 'NONE', #654, #13115, #12765 ) ;
#20925=EDGE_CURVE ( 'NONE', #20884, #20161, #18301, .T. ) ;
#20936=DIRECTION ( 'NONE',  ( 1.000000000000000000, 3.254448077276381206E-32, -1.066786462891689527E-26 ) ) ;
#20980=CIRCLE ( 'NONE', #14953, 0.5000000000000004441 ) ;
#21024=DIRECTION ( 'NONE',  ( -1.000000000000000000, 0.000000000000000000, 0.000000000000000000 ) ) ;
#21027=VERTEX_POINT ( 'NONE', #132 ) ;
#21047=DIRECTION ( 'NONE',  ( 0.000000000000000000, 0.000000000000000000, 1.000000000000000000 ) ) ;
#21050=DIRECTION ( 'NONE',  ( -7.543342432310246422E-27, -0.7071067811865516806, -0.7071067811865434649 ) ) ;
#21056=CIRCLE ( 'NONE', #10893, 2.500000000000003997 ) ;
#21074=DIRECTION ( 'NONE',  ( -1.000000000000000000, 7.100545512326564696E-57, 1.066786462891689527E-26 ) ) ;
#21099=DIRECTION ( 'NONE',  ( -1.000000000000000000, -3.254448077276381206E-32, -1.066788928082016908E-26 ) ) ;
#21116=VERTEX_POINT ( 'NONE', #16913 ) ;
#21119=DIRECTION ( 'NONE',  ( -1.066786462891689527E-26, -6.656013887802287108E-31, -1.000000000000000000 ) ) ;
#21160=ADVANCED_FACE ( 'NONE', ( #8338 ), #947, .F. ) ;
#21183=EDGE_LOOP ( 'NONE', ( #11212, #17383, #10865, #21239 ) ) ;
#21191=EDGE_CURVE ( 'NONE', #9565, #6270, #9876, .T. ) ;
#21225=DIRECTION ( 'NONE',  ( -1.000000000000000000, 0.000000000000000000, 0.000000000000000000 ) ) ;
#21239=ORIENTED_EDGE ( 'NONE', *, *, #18784, .F. ) ;
#21289=DIRECTION ( 'NONE',  ( 0.000000000000000000, -6.162975822039153854E-31, -1.000000000000000000 ) ) ;
#21295=DIRECTION ( 'NONE',  ( -1.066786462891689527E-26, -6.656013887802287108E-31, -1.000000000000000000 ) ) ;
#21308=CYLINDRICAL_SURFACE ( 'NONE', #2432, 0.2500000000000002220 ) ;
#21316=ORIENTED_EDGE ( 'NONE', *, *, #5543, .F. ) ;
#21327=ORIENTED_EDGE ( 'NONE', *, *, #22604, .T. ) ;
#21352=VERTEX_POINT ( 'NONE', #440 ) ;
#21357=EDGE_LOOP ( 'NONE', ( #1011, #3583, #14359, #19518 ) ) ;
#21371=DIRECTION ( 'NONE',  ( 1.000000000000000000, 3.254448077276381206E-32, 1.066788928082016908E-26 ) ) ;
#21383=AXIS2_PLACEMENT_3D ( 'NONE', #12079, #17503, #8463 ) ;
#21386=PLANE ( 'NONE',  #5925 ) ;
#21411=CARTESIAN_POINT ( 'NONE',  ( -6.938893903907228378E-15, 1.500000000000001332, 0.000000000000000000 ) ) ;
#21419=ORIENTED_EDGE ( 'NONE', *, *, #5841, .F. ) ;
#21428=DIRECTION ( 'NONE',  ( -1.000000000000000000, -3.254448077276381206E-32, -1.066788928082016908E-26 ) ) ;
#21439=FACE_OUTER_BOUND ( 'NONE', #19451, .T. ) ;
#21444=EDGE_LOOP ( 'NONE', ( #13098, #13380, #17013, #6912, #1102, #4495, #13704, #20710 ) ) ;
#21467=EDGE_LOOP ( 'NONE', ( #3604, #598, #22612, #1806 ) ) ;
#21488=SURFACE_STYLE_USAGE ( .BOTH. , #21713 ) ;
#21498=VERTEX_POINT ( 'NONE', #11478 ) ;
#21514=CARTESIAN_POINT ( 'NONE',  ( 24.74999999999994316, 6.938893903907228378E-14, -17.00000000000001066 ) ) ;
#21520=CYLINDRICAL_SURFACE ( 'NONE', #1776, 0.2500000000000002220 ) ;
#21566=TOROIDAL_SURFACE ( 'NONE', #5003, 0.7500000000000000000, 0.2500000000000000000 ) ;
#21570=CIRCLE ( 'NONE', #15167, 1.749999999999999778 ) ;
#21596=EDGE_CURVE ( 'NONE', #7514, #9565, #1751, .T. ) ;
#21629=EDGE_CURVE ( 'NONE', #1104, #6270, #17920, .T. ) ;
#21639=DIRECTION ( 'NONE',  ( 1.066811114794976679E-26, 0.000000000000000000, 1.000000000000000000 ) ) ;
#21670=EDGE_LOOP ( 'NONE', ( #18918, #22408, #15542, #753 ) ) ;
#21678=DIRECTION ( 'NONE',  ( -1.066786462891689527E-26, -6.656013887802287108E-31, -1.000000000000000000 ) ) ;
#21713=SURFACE_SIDE_STYLE ('',( #17946 ) ) ;
#21775=EDGE_CURVE ( 'NONE', #21498, #10194, #15634, .T. ) ;
#21780=VECTOR ( 'NONE', #20714, 1000.000000000000000 ) ;
#21785=EDGE_CURVE ( 'NONE', #7514, #21116, #20295, .T. ) ;
#21788=DIRECTION ( 'NONE',  ( 1.000000000000000000, -7.100545512326564696E-57, -1.066786462891689527E-26 ) ) ;
#21793=DIRECTION ( 'NONE',  ( 0.000000000000000000, 0.000000000000000000, 1.000000000000000000 ) ) ;
#21805=CARTESIAN_POINT ( 'NONE',  ( 22.49999999999996092, 2.000000000000043521, -17.50000000000001066 ) ) ;
#21912=TOROIDAL_SURFACE ( 'NONE', #11754, 2.250000000000000444, 0.2500000000000000000 ) ;
#21933=CONICAL_SURFACE ( 'NONE', #6510, 5.000000000000000888, 0.7853981633974430610 ) ;
#21955=ORIENTED_EDGE ( 'NONE', *, *, #1882, .F. ) ;
#21970=DIRECTION ( 'NONE',  ( -1.000000000000000000, -3.254448077276381206E-32, -1.066788928082016908E-26 ) ) ;
#21985=CARTESIAN_POINT ( 'NONE',  ( 24.99999999999995737, 2.000000000000001776, -17.49999999999998224 ) ) ;
#21988=AXIS2_PLACEMENT_3D ( 'NONE', #20699, #17376, #22458 ) ;
#21991=CARTESIAN_POINT ( 'NONE',  ( 12.49999999999995914, 2.775557561562891351E-14, -9.500000000000003553 ) ) ;
#22016=FACE_OUTER_BOUND ( 'NONE', #10766, .T. ) ;
#22026=SURFACE_STYLE_FILL_AREA ( #12977 ) ;
#22039=ORIENTED_EDGE ( 'NONE', *, *, #10792, .T. ) ;
#22074=DIRECTION ( 'NONE',  ( -1.000000000000000000, 0.000000000000000000, 0.000000000000000000 ) ) ;
#22115=AXIS2_PLACEMENT_3D ( 'NONE', #4943, #2963, #5306 ) ;
#22133=CARTESIAN_POINT ( 'NONE',  ( -1.387778780781445676E-14, 2.000000000000001776, -2.000000000000001776 ) ) ;
#22143=( NAMED_UNIT ( * ) PLANE_ANGLE_UNIT ( ) SI_UNIT ( $, .RADIAN. ) );
#22144=ORIENTED_EDGE ( 'NONE', *, *, #16535, .T. ) ;
#22155=ORIENTED_EDGE ( 'NONE', *, *, #17939, .T. ) ;
#22190=CARTESIAN_POINT ( 'NONE',  ( 24.99999999999998579, 1.249999999999987121, -17.00000000000001066 ) ) ;
#22214=CYLINDRICAL_SURFACE ( 'NONE', #9089, 0.2500000000000003331 ) ;
#22236=AXIS2_PLACEMENT_3D ( 'NONE', #13369, #5970, #11592 ) ;
#22241=DIRECTION ( 'NONE',  ( 1.066786462891689527E-26, 6.656013887802287108E-31, 1.000000000000000000 ) ) ;
#22271=VECTOR ( 'NONE', #16501, 1000.000000000000000 ) ;
#22303=ORIENTED_EDGE ( 'NONE', *, *, #4262, .T. ) ;
#22305=DIRECTION ( 'NONE',  ( -1.000000000000000000, 0.000000000000000000, 0.000000000000000000 ) ) ;
#22323=CARTESIAN_POINT ( 'NONE',  ( 0.2499999999999828748, 1.999999999999974021, -19.00000000000001066 ) ) ;
#22339=DIRECTION ( 'NONE',  ( 1.066786462891689527E-26, 6.656013887802287108E-31, 1.000000000000000000 ) ) ;
#22369=CARTESIAN_POINT ( 'NONE',  ( 22.49999999999998224, 2.000000000000001776, -1.250000000000021982 ) ) ;
#22377=DIRECTION ( 'NONE',  ( 1.000000000000000000, 0.000000000000000000, 1.066811114794976679E-26 ) ) ;
#22391=DIRECTION ( 'NONE',  ( 3.140284632889468553E-31, -1.000000000000000000, 1.734723475976804333E-15 ) ) ;
#22408=ORIENTED_EDGE ( 'NONE', *, *, #5480, .T. ) ;
#22458=DIRECTION ( 'NONE',  ( 0.000000000000000000, 0.000000000000000000, 1.000000000000000000 ) ) ;
#22469=EDGE_CURVE ( 'NONE', #800, #9468, #18677, .T. ) ;
#22498=EDGE_CURVE ( 'NONE', #19219, #20045, #16416, .T. ) ;
#22501=ORIENTED_EDGE ( 'NONE', *, *, #3266, .T. ) ;
#22542=LINE ( 'NONE', #15803, #7981 ) ;
#22543=CARTESIAN_POINT ( 'NONE',  ( -4.857225732735059864E-14, 4.500000000000059508, -17.50000000000000711 ) ) ;
#22550=CARTESIAN_POINT ( 'NONE',  ( 22.50000000000003908, 4.500000000000031974, -0.2499999999999967526 ) ) ;
#22552=VERTEX_POINT ( 'NONE', #18910 ) ;
#22554=DIRECTION ( 'NONE',  ( 1.000000000000000000, 3.254448077276381206E-32, 1.066788928082016908E-26 ) ) ;
#22604=EDGE_CURVE ( 'NONE', #882, #3485, #10801, .T. ) ;
#22612=ORIENTED_EDGE ( 'NONE', *, *, #2329, .F. ) ;
#22616=DIRECTION ( 'NONE',  ( -1.066786462891689527E-26, -6.656013887802287108E-31, -1.000000000000000000 ) ) ;
#22625=FACE_OUTER_BOUND ( 'NONE', #1945, .T. ) ;
#22631=CIRCLE ( 'NONE', #4969, 2.500000000000003553 ) ;
#22688=CARTESIAN_POINT ( 'NONE',  ( 12.49999999999995914, 0.2500000000000002220, -14.25000000000000355 ) ) ;
#22694=ADVANCED_FACE ( 'NONE', ( #3484 ), #21386, .T. ) ;
#22735=EDGE_LOOP ( 'NONE', ( #9245, #399, #8085, #8115 ) ) ;
#22739=CARTESIAN_POINT ( 'NONE',  ( 12.49999999999992362, 1.250000000000015099, -14.25000000000000178 ) ) ;
#22777=CARTESIAN_POINT ( 'NONE',  ( 0.2499999999999898137, 6.938893903907228378E-14, -17.00000000000000711 ) ) ;
#22793=EDGE_LOOP ( 'NONE', ( #20351, #4605, #2972, #20807 ) ) ;
#22842=AXIS2_PLACEMENT_3D ( 'NONE', #14041, #14159, #8866 ) ;
#22862=VECTOR ( 'NONE', #3546, 1000.000000000000000 ) ;
#22866=CARTESIAN_POINT ( 'NONE',  ( 0.2500000000000036637, 2.000000000000001776, -17.00000000000000711 ) ) ;
#22884=AXIS2_PLACEMENT_3D ( 'NONE', #11472, #434, #11248 ) ;
#22893=DIRECTION ( 'NONE',  ( 3.254448077146059901E-32, 1.000000000000000000, 6.409494854920712161E-31 ) ) ;
#22902=CARTESIAN_POINT ( 'NONE',  ( 0.2499999999999655276, 2.000000000000015543, -2.000000000000001776 ) ) ;
#22904=ORIENTED_EDGE ( 'NONE', *, *, #15391, .F. ) ;
#22905=EDGE_CURVE ( 'NONE', #16513, #10482, #3688, .T. ) ;
#22907=DIRECTION ( 'NONE',  ( 1.066786462891689527E-26, 6.656013887802287108E-31, 1.000000000000000000 ) ) ;
#22916=EDGE_LOOP ( 'NONE', ( #18242, #17711, #2520, #11499 ) ) ;
#22943=ADVANCED_FACE ( 'NONE', ( #21439 ), #12352, .T. ) ;
#22963=ORIENTED_EDGE ( 'NONE', *, *, #9477, .F. ) ;
#22965=ORIENTED_EDGE ( 'NONE', *, *, #7395, .F. ) ;
#22994=ORIENTED_EDGE ( 'NONE', *, *, #14140, .T. ) ;
#23010=CARTESIAN_POINT ( 'NONE',  ( 22.49999999999998934, 4.250000000000017764, -19.00000000000001421 ) ) ;
#23027=VERTEX_POINT ( 'NONE', #269 ) ;
#23048=EDGE_CURVE ( 'NONE', #3062, #7230, #8951, .T. ) ;
#23057=CIRCLE ( 'NONE', #11770, 0.7500000000000000000 ) ;
#23071=ORIENTED_EDGE ( 'NONE', *, *, #14240, .T. ) ;
#23082=CARTESIAN_POINT ( 'NONE',  ( 24.75000000000000355, 2.000000000000029310, -2.000000000000005329 ) ) ;
#23114=DIRECTION ( 'NONE',  ( -6.938893903907226800E-15, 0.000000000000000000, -1.000000000000000000 ) ) ;
#23172=CYLINDRICAL_SURFACE ( 'NONE', #18740, 0.2500000000000003331 ) ;
#23200=CARTESIAN_POINT ( 'NONE',  ( -2.428612866367529932E-14, 4.250000000000003553, -17.75000000000000711 ) ) ;
#23230=ADVANCED_FACE ( 'NONE', ( #1094 ), #15417, .F. ) ;
ENDSEC;
END-ISO-10303-21;
